ISO-10303-21;
HEADER;
FILE_DESCRIPTION (('STEP AP214'),
    '1' );
FILE_NAME ('Flap.step',
    '2026-10-07T18:46:32',
    ( '' ),
    ( '' ),
    'SwSTEP 2.0',
    'SolidWorks 2020',
    '' );
FILE_SCHEMA (( 'AUTOMOTIVE_DESIGN' ));
ENDSEC;

DATA;
#10=DIRECTION ( 'NONE',  ( -1.000000000000000000, 0.000000000000000000, 0.000000000000000000 ) ) ;
#39=ORIENTED_EDGE ( 'NONE', *, *, #9386, .F. ) ;
#45=ADVANCED_BREP_SHAPE_REPRESENTATION ( '', ( #20456, #17493 ), #18569 ) ;
#83=SPHERICAL_SURFACE ( 'NONE', #12076, 0.2500000000000000000 ) ;
#94=DIRECTION ( 'NONE',  ( 0.000000000000000000, 0.000000000000000000, -1.000000000000000000 ) ) ;
#115=ORIENTED_EDGE ( 'NONE', *, *, #9806, .T. ) ;
#156=CARTESIAN_POINT ( 'NONE',  ( -21.69312596654449621, 45.47506926072997402, 68.50000000000000000 ) ) ;
#171=DIRECTION ( 'NONE',  ( -1.224646799147353207E-16, -1.000000000000000000, 0.000000000000000000 ) ) ;
#174=AXIS2_PLACEMENT_3D ( 'NONE', #3147, #1221, #4718 ) ;
#185=ORIENTED_EDGE ( 'NONE', *, *, #2410, .T. ) ;
#205=CARTESIAN_POINT ( 'NONE',  ( -31.26086011588028057, 83.95073979834609190, 68.50000000000000000 ) ) ;
#218=ORIENTED_EDGE ( 'NONE', *, *, #9806, .F. ) ;
#273=EDGE_LOOP ( 'NONE', ( #3759, #6135, #19507, #342 ) ) ;
#314=ORIENTED_EDGE ( 'NONE', *, *, #1733, .T. ) ;
#338=STYLED_ITEM ( 'NONE', ( #10205 ), #45 ) ;
#342=ORIENTED_EDGE ( 'NONE', *, *, #4017, .T. ) ;
#350=MECHANICAL_DESIGN_GEOMETRIC_PRESENTATION_REPRESENTATION('',(#1426),#19311);
#354=DIRECTION ( 'NONE',  ( 0.000000000000000000, -0.000000000000000000, -1.000000000000000000 ) ) ;
#364=VECTOR ( 'NONE', #5746, 999.9999999999998863 ) ;
#413=EDGE_LOOP ( 'NONE', ( #18289, #3109, #20862 ) ) ;
#432=VECTOR ( 'NONE', #2455, 1000.000000000000000 ) ;
#485=DIRECTION ( 'NONE',  ( 0.000000000000000000, 0.000000000000000000, 1.000000000000000000 ) ) ;
#491=CARTESIAN_POINT ( 'NONE',  ( 0.000000000000000000, 0.000000000000000000, 68.50000000000000000 ) ) ;
#541=DIRECTION ( 'NONE',  ( -1.000000000000000000, 0.000000000000000000, 0.000000000000000000 ) ) ;
#573=VERTEX_POINT ( 'NONE', #16495 ) ;
#584=CARTESIAN_POINT ( 'NONE',  ( -22.16013893094044462, 45.60883947780118319, 13.75000000000000000 ) ) ;
#587=DIRECTION ( 'NONE',  ( -1.000000000000000000, 0.000000000000000000, 0.000000000000000000 ) ) ;
#633=ORIENTED_EDGE ( 'NONE', *, *, #5654, .T. ) ;
#674=AXIS2_PLACEMENT_3D ( 'NONE', #12224, #15382, #1734 ) ;
#687=AXIS2_PLACEMENT_3D ( 'NONE', #7279, #16083, #20821 ) ;
#714=AXIS2_PLACEMENT_3D ( 'NONE', #22113, #11562, #11785 ) ;
#760=ADVANCED_FACE ( 'NONE', ( #5920 ), #19446, .T. ) ;
#799=VERTEX_POINT ( 'NONE', #14842 ) ;
#816=LINE ( 'NONE', #14454, #15563 ) ;
#818=VERTEX_POINT ( 'NONE', #2898 ) ;
#824=DIRECTION ( 'NONE',  ( 0.000000000000000000, 0.000000000000000000, 1.000000000000000000 ) ) ;
#836=CIRCLE ( 'NONE', #13347, 0.2500000000000002220 ) ;
#858=CARTESIAN_POINT ( 'NONE',  ( -20.58855031337657593, 86.74083381065993592, 68.25000000000000000 ) ) ;
#859=DIRECTION ( 'NONE',  ( 0.9729678061520320442, 0.2309407893632090536, 0.000000000000000000 ) ) ;
#864=CARTESIAN_POINT ( 'NONE',  ( -32.48382792203229741, 83.71979900898287497, 68.25000000000000000 ) ) ;
#869=FACE_BOUND ( 'NONE', #11844, .T. ) ;
#906=ORIENTED_EDGE ( 'NONE', *, *, #11805, .F. ) ;
#910=CIRCLE ( 'NONE', #5944, 0.2500000000000004996 ) ;
#912=CIRCLE ( 'NONE', #14849, 0.2500000000000002220 ) ;
#935=CIRCLE ( 'NONE', #18450, 0.2500000000000013323 ) ;
#936=EDGE_CURVE ( 'NONE', #5793, #10522, #7883, .T. ) ;
#937=ORIENTED_EDGE ( 'NONE', *, *, #13020, .T. ) ;
#938=DIRECTION ( 'NONE',  ( 0.2309407893632007824, -0.9729678061520339316, 0.000000000000000000 ) ) ;
#949=CARTESIAN_POINT ( 'NONE',  ( -23.13310673709249343, 45.37789868843801599, 68.50000000000000000 ) ) ;
#956=CIRCLE ( 'NONE', #18465, 2.767785046117004377 ) ;
#991=ORIENTED_EDGE ( 'NONE', *, *, #21703, .T. ) ;
#992=CIRCLE ( 'NONE', #13505, 0.2500000000000011657 ) ;
#1069=CARTESIAN_POINT ( 'NONE',  ( -31.07535336168307083, 84.25171694722490656, 13.75000000000000000 ) ) ;
#1070=VERTEX_POINT ( 'NONE', #4000 ) ;
#1097=DIRECTION ( 'NONE',  ( 0.000000000000000000, 0.000000000000000000, 1.000000000000000000 ) ) ;
#1104=FACE_OUTER_BOUND ( 'NONE', #6482, .T. ) ;
#1111=ADVANCED_FACE ( 'NONE', ( #12353 ), #17922, .T. ) ;
#1164=DIRECTION ( 'NONE',  ( 0.000000000000000000, -0.000000000000000000, -1.000000000000000000 ) ) ;
#1174=ORIENTED_EDGE ( 'NONE', *, *, #15120, .T. ) ;
#1221=DIRECTION ( 'NONE',  ( -0.2309407893632008379, 0.9729678061520339316, 0.000000000000000000 ) ) ;
#1237=DIRECTION ( 'NONE',  ( 0.000000000000000000, 0.000000000000000000, 1.000000000000000000 ) ) ;
#1303=CIRCLE ( 'NONE', #13804, 0.2500000000000002220 ) ;
#1309=DIRECTION ( 'NONE',  ( -1.000000000000000000, 0.000000000000000000, 0.000000000000000000 ) ) ;
#1328=CIRCLE ( 'NONE', #4199, 0.2499999999999961975 ) ;
#1345=VERTEX_POINT ( 'NONE', #9056 ) ;
#1356=FILL_AREA_STYLE_COLOUR ( '', #5740 ) ;
#1379=VECTOR ( 'NONE', #19012, 1000.000000000000000 ) ;
#1426=STYLED_ITEM ( 'NONE', ( #4292 ), #20456 ) ;
#1457=CARTESIAN_POINT ( 'NONE',  ( -20.58855031337657593, 86.74083381065993592, 68.50000000000000000 ) ) ;
#1479=CARTESIAN_POINT ( 'NONE',  ( -21.71259690522456154, 45.22582864897715638, 13.75000000000000000 ) ) ;
#1493=EDGE_CURVE ( 'NONE', #13584, #6556, #956, .T. ) ;
#1568=ADVANCED_FACE ( 'NONE', ( #13623 ), #12382, .T. ) ;
#1569=CARTESIAN_POINT ( 'NONE',  ( -21.67365502786443088, 45.72430987248279166, 68.25000000000000000 ) ) ;
#1574=EDGE_CURVE ( 'NONE', #9296, #17196, #9899, .T. ) ;
#1592=VERTEX_POINT ( 'NONE', #1643 ) ;
#1630=DIRECTION ( 'NONE',  ( -1.000000000000000000, 0.000000000000000000, 0.000000000000000000 ) ) ;
#1641=CARTESIAN_POINT ( 'NONE',  ( -32.47706987357031494, 83.66206381164209915, 13.50000000000000000 ) ) ;
#1642=EDGE_CURVE ( 'NONE', #573, #8339, #21817, .T. ) ;
#1643=CARTESIAN_POINT ( 'NONE',  ( -19.85144383993102934, 42.46645089659918426, 13.49999999999999822 ) ) ;
#1652=VECTOR ( 'NONE', #14016, 999.9999999999998863 ) ;
#1654=CARTESIAN_POINT ( 'NONE',  ( -21.67365502786443088, 45.72430987248279166, 13.74999999999999822 ) ) ;
#1691=ORIENTED_EDGE ( 'NONE', *, *, #9386, .T. ) ;
#1692=SHAPE_REPRESENTATION_RELATIONSHIP ( 'NONE' , 'NONE' ,  #9142, #45 ) ;
#1695=ORIENTED_EDGE ( 'NONE', *, *, #16338, .F. ) ;
#1702=DIRECTION ( 'NONE',  ( -0.9729678061520371513, -0.2309407893631869879, 0.000000000000000000 ) ) ;
#1707=CARTESIAN_POINT ( 'NONE',  ( -21.92816239687475743, 42.46645089659918426, 68.50000000000000000 ) ) ;
#1709=CIRCLE ( 'NONE', #17792, 0.2500000000000002220 ) ;
#1717=EDGE_LOOP ( 'NONE', ( #18901, #991, #21614, #15084 ) ) ;
#1725=EDGE_CURVE ( 'NONE', #573, #15418, #7298, .T. ) ;
#1727=ADVANCED_FACE ( 'NONE', ( #2200 ), #8014, .T. ) ;
#1733=EDGE_CURVE ( 'NONE', #12990, #15862, #19803, .T. ) ;
#1734=DIRECTION ( 'NONE',  ( 1.000000000000000000, 0.000000000000000000, 0.000000000000000000 ) ) ;
#1770=DIRECTION ( 'NONE',  ( 0.000000000000000000, 0.000000000000000000, 1.000000000000000000 ) ) ;
#1791=DIRECTION ( 'NONE',  ( -1.224646799147353207E-16, -1.000000000000000000, 0.000000000000000000 ) ) ;
#1838=CYLINDRICAL_SURFACE ( 'NONE', #10973, 0.2500000000000002220 ) ;
#1876=DIRECTION ( 'NONE',  ( -1.000000000000000000, 0.000000000000000000, 0.000000000000000000 ) ) ;
#1887=EDGE_CURVE ( 'NONE', #9421, #5793, #836, .T. ) ;
#1922=DIRECTION ( 'NONE',  ( -0.000000000000000000, -0.000000000000000000, -1.000000000000000000 ) ) ;
#1934=LINE ( 'NONE', #5098, #4171 ) ;
#2013=AXIS2_PLACEMENT_3D ( 'NONE', #2483, #14775, #10 ) ;
#2041=ADVANCED_FACE ( 'NONE', ( #11794 ), #11210, .T. ) ;
#2091=EDGE_LOOP ( 'NONE', ( #18512, #12254, #12155, #5768 ) ) ;
#2120=LINE ( 'NONE', #8955, #432 ) ;
#2124=EDGE_LOOP ( 'NONE', ( #9690, #21999, #1691, #21101 ) ) ;
#2130=AXIS2_PLACEMENT_3D ( 'NONE', #10660, #354, #15788 ) ;
#2147=FACE_OUTER_BOUND ( 'NONE', #2934, .T. ) ;
#2160=DIRECTION ( 'NONE',  ( -1.000000000000000000, 0.000000000000000000, 0.000000000000000000 ) ) ;
#2162=ORIENTED_EDGE ( 'NONE', *, *, #8500, .F. ) ;
#2165=FACE_OUTER_BOUND ( 'NONE', #18868, .T. ) ;
#2186=AXIS2_PLACEMENT_3D ( 'NONE', #4661, #11471, #2636 ) ;
#2188=ORIENTED_EDGE ( 'NONE', *, *, #9154, .F. ) ;
#2200=FACE_OUTER_BOUND ( 'NONE', #12642, .T. ) ;
#2263=EDGE_LOOP ( 'NONE', ( #18702, #12930, #6688, #1174 ) ) ;
#2269=VERTEX_POINT ( 'NONE', #17575 ) ;
#2282=ORIENTED_EDGE ( 'NONE', *, *, #7746, .F. ) ;
#2297=DIRECTION ( 'NONE',  ( -0.2309407893632113573, 0.9729678061520313781, 0.000000000000000000 ) ) ;
#2346=AXIS2_PLACEMENT_3D ( 'NONE', #17140, #8866, #12095 ) ;
#2351=AXIS2_PLACEMENT_3D ( 'NONE', #4186, #21210, #19741 ) ;
#2353=AXIS2_PLACEMENT_3D ( 'NONE', #13359, #20312, #13789 ) ;
#2362=AXIS2_PLACEMENT_3D ( 'NONE', #2476, #21182, #18010 ) ;
#2410=EDGE_CURVE ( 'NONE', #5908, #21506, #13293, .T. ) ;
#2419=DIRECTION ( 'NONE',  ( -1.000000000000000000, 0.000000000000000000, 0.000000000000000000 ) ) ;
#2422=DIRECTION ( 'NONE',  ( -1.000000000000000000, 0.000000000000000000, 0.000000000000000000 ) ) ;
#2455=DIRECTION ( 'NONE',  ( -0.000000000000000000, -0.000000000000000000, 1.000000000000000000 ) ) ;
#2476=CARTESIAN_POINT ( 'NONE',  ( -21.92816239687475743, 42.46645089659918426, 68.25000000000000000 ) ) ;
#2483=CARTESIAN_POINT ( 'NONE',  ( -21.92816239687475743, 42.46645089659918426, 13.50000000000000000 ) ) ;
#2491=ADVANCED_FACE ( 'NONE', ( #12009 ), #8779, .T. ) ;
#2498=CARTESIAN_POINT ( 'NONE',  ( -31.31859531322107060, 84.19398174988410233, 13.75000000000000000 ) ) ;
#2514=ORIENTED_EDGE ( 'NONE', *, *, #2945, .T. ) ;
#2515=CIRCLE ( 'NONE', #10749, 0.2499999999999985012 ) ;
#2518=CARTESIAN_POINT ( 'NONE',  ( -31.26086011588027347, 83.95073979834609190, 13.75000000000000000 ) ) ;
#2555=CARTESIAN_POINT ( 'NONE',  ( -32.29156311937310164, 83.96304096052089960, 68.50000000000000000 ) ) ;
#2562=DIRECTION ( 'NONE',  ( 0.000000000000000000, -0.000000000000000000, -1.000000000000000000 ) ) ;
#2566=DIRECTION ( 'NONE',  ( 0.000000000000000000, -0.000000000000000000, -1.000000000000000000 ) ) ;
#2610=DIRECTION ( 'NONE',  ( -1.000000000000000000, 0.000000000000000000, 0.000000000000000000 ) ) ;
#2636=DIRECTION ( 'NONE',  ( -1.000000000000000000, 0.000000000000000000, 0.000000000000000000 ) ) ;
#2648=EDGE_CURVE ( 'NONE', #13584, #8339, #17567, .T. ) ;
#2654=ORIENTED_EDGE ( 'NONE', *, *, #6389, .F. ) ;
#2663=VERTEX_POINT ( 'NONE', #2498 ) ;
#2674=ORIENTED_EDGE ( 'NONE', *, *, #20183, .T. ) ;
#2675=CARTESIAN_POINT ( 'NONE',  ( -23.61959064016851073, 45.26242829375641463, 68.25000000000000000 ) ) ;
#2681=ADVANCED_FACE ( 'NONE', ( #2165 ), #7439, .T. ) ;
#2717=CARTESIAN_POINT ( 'NONE',  ( -24.69594744299175915, 42.46645089659918426, 13.50000000000000000 ) ) ;
#2733=CARTESIAN_POINT ( 'NONE',  ( -19.16037735075775217, 42.46645089659918426, 68.25000000000000000 ) ) ;
#2744=DIRECTION ( 'NONE',  ( -1.000000000000000000, 0.000000000000000000, 0.000000000000000000 ) ) ;
#2752=AXIS2_PLACEMENT_3D ( 'NONE', #20154, #9226, #5778 ) ;
#2787=AXIS2_PLACEMENT_3D ( 'NONE', #10728, #9147, #10502 ) ;
#2848=DIRECTION ( 'NONE',  ( -0.000000000000000000, -0.000000000000000000, -1.000000000000000000 ) ) ;
#2870=CARTESIAN_POINT ( 'NONE',  ( -23.61959064016851073, 45.26242829375641463, 68.25000000000000000 ) ) ;
#2898=CARTESIAN_POINT ( 'NONE',  ( -23.75488095381848197, 42.46645089659918426, 68.25000000000000000 ) ) ;
#2934=EDGE_LOOP ( 'NONE', ( #13699, #7776, #8142, #5644 ) ) ;
#2939=( NAMED_UNIT ( * ) PLANE_ANGLE_UNIT ( ) SI_UNIT ( $, .RADIAN. ) );
#2945=EDGE_CURVE ( 'NONE', #16071, #15168, #18712, .T. ) ;
#2958=ORIENTED_EDGE ( 'NONE', *, *, #10719, .F. ) ;
#3005=CARTESIAN_POINT ( 'NONE',  ( -21.92816239687475743, 42.46645089659918426, 13.50000000000000000 ) ) ;
#3066=EDGE_CURVE ( 'NONE', #12192, #799, #21912, .T. ) ;
#3081=CARTESIAN_POINT ( 'NONE',  ( -20.10144383993102934, 42.46645089659918426, 13.74999999999999822 ) ) ;
#3096=CIRCLE ( 'NONE', #2013, 2.767785046117004377 ) ;
#3105=CIRCLE ( 'NONE', #12137, 1.826718556943725202 ) ;
#3109=ORIENTED_EDGE ( 'NONE', *, *, #5282, .T. ) ;
#3123=EDGE_LOOP ( 'NONE', ( #21386, #5828, #8706, #19486 ) ) ;
#3147=CARTESIAN_POINT ( 'NONE',  ( -32.23382792203229741, 83.71979900898287497, 68.25000000000000000 ) ) ;
#3151=PLANE ( 'NONE',  #8499 ) ;
#3166=ORIENTED_EDGE ( 'NONE', *, *, #2945, .F. ) ;
#3176=CIRCLE ( 'NONE', #11740, 0.2500000000000002220 ) ;
#3184=TOROIDAL_SURFACE ( 'NONE', #11033, 2.076718556943726313, 0.2500000000000000000 ) ;
#3230=AXIS2_PLACEMENT_3D ( 'NONE', #19498, #3972, #17817 ) ;
#3233=ORIENTED_EDGE ( 'NONE', *, *, #12770, .T. ) ;
#3240=VERTEX_POINT ( 'NONE', #11296 ) ;
#3266=AXIS2_PLACEMENT_3D ( 'NONE', #4769, #19999, #11572 ) ;
#3267=ORIENTED_EDGE ( 'NONE', *, *, #10098, .T. ) ;
#3270=SURFACE_STYLE_USAGE ( .BOTH. , #19725 ) ;
#3271=EDGE_CURVE ( 'NONE', #573, #7129, #6599, .T. ) ;
#3295=FACE_OUTER_BOUND ( 'NONE', #17576, .T. ) ;
#3308=DIRECTION ( 'NONE',  ( -1.000000000000000000, 0.000000000000000000, 0.000000000000000000 ) ) ;
#3313=ORIENTED_EDGE ( 'NONE', *, *, #12905, .T. ) ;
#3331=FACE_OUTER_BOUND ( 'NONE', #7926, .T. ) ;
#3337=DIRECTION ( 'NONE',  ( 0.9729678061520345977, 0.2309407893631976461, 0.000000000000000000 ) ) ;
#3344=FACE_OUTER_BOUND ( 'NONE', #19612, .T. ) ;
#3346=ORIENTED_EDGE ( 'NONE', *, *, #2648, .T. ) ;
#3363=ORIENTED_EDGE ( 'NONE', *, *, #19287, .T. ) ;
#3364=DIRECTION ( 'NONE',  ( 0.9729678061520319332, 0.2309407893632090258, 0.000000000000000000 ) ) ;
#3392=ORIENTED_EDGE ( 'NONE', *, *, #4858, .F. ) ;
#3405=CARTESIAN_POINT ( 'NONE',  ( -23.61959064016851073, 45.26242829375641463, 68.50000000000000000 ) ) ;
#3407=CIRCLE ( 'NONE', #15890, 2.767785046117004377 ) ;
#3443=LINE ( 'NONE', #1641, #9245 ) ;
#3482=AXIS2_PLACEMENT_3D ( 'NONE', #8882, #19062, #17484 ) ;
#3506=CARTESIAN_POINT ( 'NONE',  ( -23.36078716634399655, 44.83461903493144973, 13.50000000000000000 ) ) ;
#3513=ORIENTED_EDGE ( 'NONE', *, *, #4482, .T. ) ;
#3536=CIRCLE ( 'NONE', #3482, 3.017785046117004377 ) ;
#3598=CIRCLE ( 'NONE', #16791, 0.2500000000000011657 ) ;
#3612=FACE_OUTER_BOUND ( 'NONE', #3123, .T. ) ;
#3616=DIRECTION ( 'NONE',  ( 0.000000000000000000, -0.000000000000000000, -1.000000000000000000 ) ) ;
#3634=ADVANCED_FACE ( 'NONE', ( #6164 ), #4248, .T. ) ;
#3652=ORIENTED_EDGE ( 'NONE', *, *, #19586, .T. ) ;
#3704=FACE_OUTER_BOUND ( 'NONE', #17459, .T. ) ;
#3715=ADVANCED_FACE ( 'NONE', ( #18744 ), #7829, .T. ) ;
#3724=AXIS2_PLACEMENT_3D ( 'NONE', #20435, #4660, #3308 ) ;
#3726=DIRECTION ( 'NONE',  ( 0.000000000000000000, 0.000000000000000000, 1.000000000000000000 ) ) ;
#3730=EDGE_LOOP ( 'NONE', ( #8356, #5401, #4211, #6254 ) ) ;
#3749=ADVANCED_FACE ( 'NONE', ( #1104 ), #14753, .F. ) ;
#3758=FACE_BOUND ( 'NONE', #17109, .T. ) ;
#3759=ORIENTED_EDGE ( 'NONE', *, *, #3271, .F. ) ;
#3764=DIRECTION ( 'NONE',  ( 0.000000000000000000, 0.000000000000000000, 1.000000000000000000 ) ) ;
#3772=DIRECTION ( 'NONE',  ( 0.000000000000000000, 0.000000000000000000, 1.000000000000000000 ) ) ;
#3773=DIRECTION ( 'NONE',  ( 0.000000000000000000, 0.000000000000000000, 1.000000000000000000 ) ) ;
#3781=ORIENTED_EDGE ( 'NONE', *, *, #10455, .F. ) ;
#3786=CARTESIAN_POINT ( 'NONE',  ( -18.91037735075775217, 42.46645089659918426, 13.74999999999999822 ) ) ;
#3855=CARTESIAN_POINT ( 'NONE',  ( -21.92816239687475743, 42.46645089659918426, 13.74999999999999822 ) ) ;
#3906=AXIS2_PLACEMENT_3D ( 'NONE', #5246, #3773, #1876 ) ;
#3907=ORIENTED_EDGE ( 'NONE', *, *, #10331, .F. ) ;
#3908=EDGE_LOOP ( 'NONE', ( #9178, #10832, #16671, #20587 ) ) ;
#3926=ORIENTED_EDGE ( 'NONE', *, *, #16346, .T. ) ;
#3944=ADVANCED_FACE ( 'NONE', ( #12374 ), #3184, .T. ) ;
#3951=COLOUR_RGB ( '', 0.08235294, 0.09019608, 0.10196078) ;
#3972=DIRECTION ( 'NONE',  ( 0.000000000000000000, -1.000000000000000000, 0.000000000000000000 ) ) ;
#3974=CARTESIAN_POINT ( 'NONE',  ( -32.23382792203229741, 83.71979900898287497, 13.75000000000000000 ) ) ;
#3977=DIRECTION ( 'NONE',  ( 0.000000000000000000, -0.000000000000000000, -1.000000000000000000 ) ) ;
#4000=CARTESIAN_POINT ( 'NONE',  ( -24.94594744299175915, 42.46645089659918426, 13.74999999999999822 ) ) ;
#4001=DIRECTION ( 'NONE',  ( 0.000000000000000000, -1.000000000000000000, 0.000000000000000000 ) ) ;
#4005=DIRECTION ( 'NONE',  ( 0.000000000000000000, 1.000000000000000000, -0.000000000000000000 ) ) ;
#4017=EDGE_CURVE ( 'NONE', #16466, #7129, #10610, .T. ) ;
#4021=EDGE_LOOP ( 'NONE', ( #15747, #14061, #12694, #2654 ) ) ;
#4049=DIRECTION ( 'NONE',  ( 1.000000000000000000, 0.000000000000000000, 0.000000000000000000 ) ) ;
#4062=ORIENTED_EDGE ( 'NONE', *, *, #18303, .T. ) ;
#4064=ORIENTED_EDGE ( 'NONE', *, *, #21581, .F. ) ;
#4078=LINE ( 'NONE', #7559, #18845 ) ;
#4079=ORIENTED_EDGE ( 'NONE', *, *, #6560, .F. ) ;
#4120=DIRECTION ( 'NONE',  ( 0.2309407893632139108, -0.9729678061520308230, 0.000000000000000000 ) ) ;
#4157=LINE ( 'NONE', #14333, #7544 ) ;
#4171=VECTOR ( 'NONE', #17267, 1000.000000000000000 ) ;
#4186=CARTESIAN_POINT ( 'NONE',  ( -21.92816239687475743, 42.46645089659918426, 68.25000000000000000 ) ) ;
#4199=AXIS2_PLACEMENT_3D ( 'NONE', #5318, #10451, #20522 ) ;
#4211=ORIENTED_EDGE ( 'NONE', *, *, #21024, .T. ) ;
#4246=CIRCLE ( 'NONE', #22116, 3.017785046117004377 ) ;
#4248=CYLINDRICAL_SURFACE ( 'NONE', #14979, 0.2500000000000001665 ) ;
#4252=AXIS2_PLACEMENT_3D ( 'NONE', #20744, #3726, #10875 ) ;
#4253=CARTESIAN_POINT ( 'NONE',  ( -24.69594744299175915, 42.46645089659918426, 13.74999999999999822 ) ) ;
#4287=AXIS2_PLACEMENT_3D ( 'NONE', #8602, #22151, #15175 ) ;
#4292=PRESENTATION_STYLE_ASSIGNMENT (( #19619 ) ) ;
#4317=FACE_OUTER_BOUND ( 'NONE', #10397, .T. ) ;
#4384=CARTESIAN_POINT ( 'NONE',  ( -23.33295178540679160, 45.13732965806239150, 68.25000000000000000 ) ) ;
#4418=DIRECTION ( 'NONE',  ( -1.000000000000000000, 0.000000000000000000, 0.000000000000000000 ) ) ;
#4451=DIRECTION ( 'NONE',  ( -0.2309407893632008379, 0.9729678061520339316, 0.000000000000000000 ) ) ;
#4482=EDGE_CURVE ( 'NONE', #3240, #10960, #21384, .T. ) ;
#4514=ORIENTED_EDGE ( 'NONE', *, *, #10465, .F. ) ;
#4523=DIRECTION ( 'NONE',  ( 1.000000000000000000, 0.000000000000000000, 0.000000000000000000 ) ) ;
#4540=CARTESIAN_POINT ( 'NONE',  ( -32.23382792203229741, 83.71979900898287497, 68.25000000000000000 ) ) ;
#4547=AXIS2_PLACEMENT_3D ( 'NONE', #16757, #8609, #3337 ) ;
#4560=EDGE_CURVE ( 'NONE', #16071, #20875, #13153, .T. ) ;
#4575=LINE ( 'NONE', #19685, #7366 ) ;
#4583=DIRECTION ( 'NONE',  ( 1.000000000000000000, 0.000000000000000000, 6.938893903907222067E-15 ) ) ;
#4608=ADVANCED_FACE ( 'NONE', ( #3331 ), #83, .T. ) ;
#4620=UNCERTAINTY_MEASURE_WITH_UNIT (LENGTH_MEASURE( 1.000000000000000082E-05 ), #13765, 'distance_accuracy_value', 'NONE');
#4660=DIRECTION ( 'NONE',  ( 0.000000000000000000, 0.000000000000000000, 1.000000000000000000 ) ) ;
#4661=CARTESIAN_POINT ( 'NONE',  ( -23.61959064016851073, 45.26242829375641463, 68.25000000000000000 ) ) ;
#4700=ORIENTED_EDGE ( 'NONE', *, *, #20532, .F. ) ;
#4718=DIRECTION ( 'NONE',  ( 0.9729678061520339316, 0.2309407893632007824, 0.000000000000000000 ) ) ;
#4739=AXIS2_PLACEMENT_3D ( 'NONE', #10303, #1791, #13736 ) ;
#4750=CARTESIAN_POINT ( 'NONE',  ( -21.92816239687475743, 42.46645089659918426, 13.74999999999999822 ) ) ;
#4769=CARTESIAN_POINT ( 'NONE',  ( -20.53081511603577169, 86.49759185912192549, 68.25000000000000000 ) ) ;
#4835=TOROIDAL_SURFACE ( 'NONE', #9127, 2.767785046117003489, 0.2500000000000000000 ) ;
#4841=CARTESIAN_POINT ( 'NONE',  ( -23.49018890325625364, 45.04852366434393218, 68.25000000000000000 ) ) ;
#4858=EDGE_CURVE ( 'NONE', #15168, #14169, #912, .T. ) ;
#4872=DIRECTION ( 'NONE',  ( -1.000000000000000000, 0.000000000000000000, 0.000000000000000000 ) ) ;
#4884=EDGE_LOOP ( 'NONE', ( #9073, #1695, #9405, #11477 ) ) ;
#4920=ORIENTED_EDGE ( 'NONE', *, *, #4560, .F. ) ;
#4928=CARTESIAN_POINT ( 'NONE',  ( -31.26086011588028057, 83.95073979834610611, 13.75000000000000000 ) ) ;
#4987=CARTESIAN_POINT ( 'NONE',  ( -21.92816239687475743, 42.46645089659918426, 13.74999999999999822 ) ) ;
#4996=ADVANCED_FACE ( 'NONE', ( #10104 ), #13665, .T. ) ;
#4998=ORIENTED_EDGE ( 'NONE', *, *, #19287, .F. ) ;
#5012=DIRECTION ( 'NONE',  ( -1.000000000000000000, 0.000000000000000000, 0.000000000000000000 ) ) ;
#5035=VERTEX_POINT ( 'NONE', #10435 ) ;
#5058=DIRECTION ( 'NONE',  ( -0.000000000000000000, -0.000000000000000000, -1.000000000000000000 ) ) ;
#5068=DIRECTION ( 'NONE',  ( -0.000000000000000000, -0.000000000000000000, -1.000000000000000000 ) ) ;
#5098=CARTESIAN_POINT ( 'NONE',  ( -21.91689697940243775, 45.66657467514198743, 68.50000000000000000 ) ) ;
#5113=VERTEX_POINT ( 'NONE', #10650 ) ;
#5159=DIRECTION ( 'NONE',  ( 0.9729678061520339316, 0.2309407893632007824, 0.000000000000000000 ) ) ;
#5168=ORIENTED_EDGE ( 'NONE', *, *, #21884, .F. ) ;
#5180=DIRECTION ( 'NONE',  ( 1.000000000000000000, 0.000000000000000000, 0.000000000000000000 ) ) ;
#5246=CARTESIAN_POINT ( 'NONE',  ( -21.92816239687475743, 42.46645089659918426, 68.50000000000000000 ) ) ;
#5282=EDGE_CURVE ( 'NONE', #5035, #5552, #935, .T. ) ;
#5292=ORIENTED_EDGE ( 'NONE', *, *, #20301, .T. ) ;
#5318=CARTESIAN_POINT ( 'NONE',  ( -31.26086011588028057, 83.95073979834609190, 68.25000000000000000 ) ) ;
#5375=EDGE_CURVE ( 'NONE', #20875, #12990, #18093, .T. ) ;
#5396=DIRECTION ( 'NONE',  ( 0.000000000000000000, -1.000000000000000000, 0.000000000000000000 ) ) ;
#5399=ORIENTED_EDGE ( 'NONE', *, *, #16031, .T. ) ;
#5401=ORIENTED_EDGE ( 'NONE', *, *, #10452, .T. ) ;
#5448=ORIENTED_EDGE ( 'NONE', *, *, #16031, .F. ) ;
#5477=ORIENTED_EDGE ( 'NONE', *, *, #12770, .F. ) ;
#5507=ORIENTED_EDGE ( 'NONE', *, *, #5662, .T. ) ;
#5552=VERTEX_POINT ( 'NONE', #5669 ) ;
#5562=DIRECTION ( 'NONE',  ( -0.2309407893632008379, 0.9729678061520339316, -0.000000000000000000 ) ) ;
#5567=CARTESIAN_POINT ( 'NONE',  ( -11.70301280599631433, -2.777792850139019443, 13.74999999999999822 ) ) ;
#5608=DIRECTION ( 'NONE',  ( 0.000000000000000000, 0.000000000000000000, 1.000000000000000000 ) ) ;
#5644=ORIENTED_EDGE ( 'NONE', *, *, #12702, .F. ) ;
#5654=EDGE_CURVE ( 'NONE', #20520, #16071, #10218, .T. ) ;
#5662=EDGE_CURVE ( 'NONE', #5035, #18477, #9509, .T. ) ;
#5669=CARTESIAN_POINT ( 'NONE',  ( -31.26086011588028057, 83.95073979834610611, 13.50000000000000000 ) ) ;
#5686=CIRCLE ( 'NONE', #17757, 0.2500000000000002220 ) ;
#5721=DIRECTION ( 'NONE',  ( -0.2309407893632113573, 0.9729678061520313781, 0.000000000000000000 ) ) ;
#5740=COLOUR_RGB ( '', 0.08235294, 0.09019608, 0.10196078) ;
#5746=DIRECTION ( 'NONE',  ( 0.2309407893632117181, -0.9729678061520313781, -0.000000000000000000 ) ) ;
#5765=EDGE_CURVE ( 'NONE', #12192, #1070, #4575, .T. ) ;
#5768=ORIENTED_EDGE ( 'NONE', *, *, #1887, .T. ) ;
#5778=DIRECTION ( 'NONE',  ( -1.000000000000000000, 0.000000000000000000, 0.000000000000000000 ) ) ;
#5793=VERTEX_POINT ( 'NONE', #864 ) ;
#5797=LINE ( 'NONE', #12248, #9497 ) ;
#5810=AXIS2_PLACEMENT_3D ( 'NONE', #4750, #2848, #11550 ) ;
#5817=EDGE_CURVE ( 'NONE', #6556, #22161, #3407, .T. ) ;
#5820=VERTEX_POINT ( 'NONE', #21600 ) ;
#5821=CARTESIAN_POINT ( 'NONE',  ( -21.91689697940243775, 45.66657467514198743, 13.75000000000000000 ) ) ;
#5828=ORIENTED_EDGE ( 'NONE', *, *, #5765, .T. ) ;
#5843=ORIENTED_EDGE ( 'NONE', *, *, #5654, .F. ) ;
#5908=VERTEX_POINT ( 'NONE', #18898 ) ;
#5920=FACE_OUTER_BOUND ( 'NONE', #18029, .T. ) ;
#5934=CARTESIAN_POINT ( 'NONE',  ( -23.61959064016851073, 45.26242829375641463, 68.50000000000000000 ) ) ;
#5944=AXIS2_PLACEMENT_3D ( 'NONE', #13682, #20186, #14920 ) ;
#5960=CIRCLE ( 'NONE', #14139, 0.2500000000000004996 ) ;
#5973=EDGE_CURVE ( 'NONE', #16645, #16312, #13626, .T. ) ;
#5976=VECTOR ( 'NONE', #21849, 1000.000000000000000 ) ;
#5978=CARTESIAN_POINT ( 'NONE',  ( -23.36959064016851073, 45.26242829375641463, 68.25000000000000000 ) ) ;
#5981=SURFACE_SIDE_STYLE ('',( #12991 ) ) ;
#5990=LINE ( 'NONE', #10796, #18272 ) ;
#5996=AXIS2_PLACEMENT_3D ( 'NONE', #14517, #12720, #4583 ) ;
#6025=AXIS2_PLACEMENT_3D ( 'NONE', #1569, #5058, #21957 ) ;
#6101=DIRECTION ( 'NONE',  ( -0.000000000000000000, -0.000000000000000000, -1.000000000000000000 ) ) ;
#6114=DIRECTION ( 'NONE',  ( -1.224646799147353207E-16, -1.000000000000000000, 0.000000000000000000 ) ) ;
#6135=ORIENTED_EDGE ( 'NONE', *, *, #1642, .T. ) ;
#6164=FACE_OUTER_BOUND ( 'NONE', #8469, .T. ) ;
#6202=DIRECTION ( 'NONE',  ( 0.000000000000000000, 0.000000000000000000, 1.000000000000000000 ) ) ;
#6210=VERTEX_POINT ( 'NONE', #3081 ) ;
#6254=ORIENTED_EDGE ( 'NONE', *, *, #5973, .T. ) ;
#6311=AXIS2_PLACEMENT_3D ( 'NONE', #21773, #10123, #8116 ) ;
#6347=ORIENTED_EDGE ( 'NONE', *, *, #1574, .T. ) ;
#6352=VECTOR ( 'NONE', #18662, 1000.000000000000000 ) ;
#6355=AXIS2_PLACEMENT_3D ( 'NONE', #9233, #16247, #11118 ) ;
#6389=EDGE_CURVE ( 'NONE', #3240, #5820, #17502, .T. ) ;
#6416=EDGE_LOOP ( 'NONE', ( #16145, #16205, #21599, #4998 ) ) ;
#6439=CARTESIAN_POINT ( 'NONE',  ( -20.10144383993102934, 42.46645089659918426, 68.50000000000000000 ) ) ;
#6441=CARTESIAN_POINT ( 'NONE',  ( -21.92816239687475743, 42.46645089659918426, 68.50000000000000000 ) ) ;
#6458=DIRECTION ( 'NONE',  ( 0.000000000000000000, -1.000000000000000000, 0.000000000000000000 ) ) ;
#6472=AXIS2_PLACEMENT_3D ( 'NONE', #17027, #1702, #8214 ) ;
#6482=EDGE_LOOP ( 'NONE', ( #633, #2514, #15506, #7506 ) ) ;
#6495=DIRECTION ( 'NONE',  ( 0.000000000000000000, 0.000000000000000000, 1.000000000000000000 ) ) ;
#6514=CIRCLE ( 'NONE', #5810, 3.017785046117004377 ) ;
#6535=AXIS2_PLACEMENT_3D ( 'NONE', #10967, #21174, #11180 ) ;
#6540=SURFACE_STYLE_FILL_AREA ( #8204 ) ;
#6556=VERTEX_POINT ( 'NONE', #2717 ) ;
#6560=EDGE_CURVE ( 'NONE', #1592, #20918, #18798, .T. ) ;
#6599=CIRCLE ( 'NONE', #8729, 0.2499999999999977796 ) ;
#6600=CARTESIAN_POINT ( 'NONE',  ( -21.67365502786443088, 45.72430987248279166, 68.25000000000000000 ) ) ;
#6645=CYLINDRICAL_SURFACE ( 'NONE', #14952, 1.826718556943725202 ) ;
#6688=ORIENTED_EDGE ( 'NONE', *, *, #5375, .T. ) ;
#6726=TOROIDAL_SURFACE ( 'NONE', #18131, 2.767785046117003489, 0.2500000000000000000 ) ;
#6789=FACE_OUTER_BOUND ( 'NONE', #17388, .T. ) ;
#6799=ORIENTED_EDGE ( 'NONE', *, *, #19837, .T. ) ;
#6897=APPLICATION_CONTEXT ( 'automotive_design' ) ;
#6967=ORIENTED_EDGE ( 'NONE', *, *, #14773, .F. ) ;
#6999=FACE_OUTER_BOUND ( 'NONE', #1717, .T. ) ;
#7003=FACE_OUTER_BOUND ( 'NONE', #4021, .T. ) ;
#7010=CARTESIAN_POINT ( 'NONE',  ( -18.91037735075775217, 42.46645089659918426, 68.25000000000000000 ) ) ;
#7026=VECTOR ( 'NONE', #16372, 1000.000000000000000 ) ;
#7027=EDGE_LOOP ( 'NONE', ( #17868, #13662, #21501, #17323 ) ) ;
#7029=CARTESIAN_POINT ( 'NONE',  ( -32.23382792203229741, 83.71979900898287497, 68.25000000000000000 ) ) ;
#7042=EDGE_CURVE ( 'NONE', #9421, #10522, #9462, .T. ) ;
#7046=CARTESIAN_POINT ( 'NONE',  ( -11.94625475753432120, -2.835528047479821900, 13.74999999999999822 ) ) ;
#7129=VERTEX_POINT ( 'NONE', #8933 ) ;
#7141=PRODUCT_DEFINITION ( 'UNKNOWN', '', #12987, #16911 ) ;
#7148=CARTESIAN_POINT ( 'NONE',  ( -23.61959064016851073, 45.26242829375641463, 68.50000000000000000 ) ) ;
#7173=CARTESIAN_POINT ( 'NONE',  ( -32.47706987357030073, 83.66206381164208494, 68.25000000000000000 ) ) ;
#7195=CIRCLE ( 'NONE', #21142, 2.076718556943725424 ) ;
#7219=LINE ( 'NONE', #17698, #1652 ) ;
#7223=DIRECTION ( 'NONE',  ( 0.000000000000000000, 0.000000000000000000, 1.000000000000000000 ) ) ;
#7271=CARTESIAN_POINT ( 'NONE',  ( -19.85144383993102934, 42.46645089659918426, 68.50000000000000000 ) ) ;
#7279=CARTESIAN_POINT ( 'NONE',  ( -24.00488095381848197, 42.46645089659918426, 68.25000000000000000 ) ) ;
#7298=CIRCLE ( 'NONE', #9428, 0.2500000000000002220 ) ;
#7300=DIRECTION ( 'NONE',  ( 0.8556185176499236933, 0.5176069476490314791, 0.000000000000000000 ) ) ;
#7322=FACE_OUTER_BOUND ( 'NONE', #15277, .T. ) ;
#7325=DIRECTION ( 'NONE',  ( -0.2309407893632008379, 0.9729678061520339316, 0.000000000000000000 ) ) ;
#7333=CARTESIAN_POINT ( 'NONE',  ( -21.92816239687475743, 42.46645089659918426, 68.25000000000000000 ) ) ;
#7339=DIRECTION ( 'NONE',  ( -1.000000000000000000, 0.000000000000000000, 0.000000000000000000 ) ) ;
#7350=FACE_OUTER_BOUND ( 'NONE', #273, .T. ) ;
#7353=CARTESIAN_POINT ( 'NONE',  ( -21.92816239687475743, 42.46645089659918426, 13.74999999999999822 ) ) ;
#7366=VECTOR ( 'NONE', #2562, 1000.000000000000000 ) ;
#7437=FACE_OUTER_BOUND ( 'NONE', #18252, .T. ) ;
#7439=SPHERICAL_SURFACE ( 'NONE', #21517, 0.2500000000000000000 ) ;
#7452=CYLINDRICAL_SURFACE ( 'NONE', #2752, 0.2500000000000002220 ) ;
#7481=ORIENTED_EDGE ( 'NONE', *, *, #4560, .T. ) ;
#7506=ORIENTED_EDGE ( 'NONE', *, *, #11521, .T. ) ;
#7514=EDGE_LOOP ( 'NONE', ( #12855, #4920, #5843, #20909, #19702 ) ) ;
#7529=ADVANCED_FACE ( 'NONE', ( #10471 ), #4835, .T. ) ;
#7544=VECTOR ( 'NONE', #21189, 999.9999999999998863 ) ;
#7559=CARTESIAN_POINT ( 'NONE',  ( -31.01761816434226660, 84.00847499568689614, 68.50000000000000000 ) ) ;
#7590=CIRCLE ( 'NONE', #12907, 2.767785046117004377 ) ;
#7594=EDGE_LOOP ( 'NONE', ( #19317, #20342, #10359, #12955 ) ) ;
#7595=DIRECTION ( 'NONE',  ( 0.9729678061520313781, 0.2309407893632113573, 0.000000000000000000 ) ) ;
#7663=ORIENTED_EDGE ( 'NONE', *, *, #10504, .F. ) ;
#7679=CARTESIAN_POINT ( 'NONE',  ( -22.16013893094044462, 45.60883947780118319, 13.50000000000000000 ) ) ;
#7693=EDGE_CURVE ( 'NONE', #818, #7934, #17341, .T. ) ;
#7716=EDGE_CURVE ( 'NONE', #20875, #16466, #12894, .T. ) ;
#7746=EDGE_CURVE ( 'NONE', #10522, #9296, #816, .T. ) ;
#7762=CARTESIAN_POINT ( 'NONE',  ( -24.00488095381848197, 42.46645089659918426, 13.74999999999999822 ) ) ;
#7771=CARTESIAN_POINT ( 'NONE',  ( -21.92816239687475743, 42.46645089659918426, 13.50000000000000000 ) ) ;
#7776=ORIENTED_EDGE ( 'NONE', *, *, #12619, .F. ) ;
#7778=AXIS2_PLACEMENT_3D ( 'NONE', #16438, #11943, #15519 ) ;
#7800=DIRECTION ( 'NONE',  ( 0.000000000000000000, 0.000000000000000000, 1.000000000000000000 ) ) ;
#7806=DIRECTION ( 'NONE',  ( -0.000000000000000000, -0.000000000000000000, -1.000000000000000000 ) ) ;
#7829=TOROIDAL_SURFACE ( 'NONE', #4252, 2.767785046117003489, 0.2500000000000000000 ) ;
#7832=CARTESIAN_POINT ( 'NONE',  ( -20.53081511603577525, 86.49759185912193971, 13.75000000000000000 ) ) ;
#7836=CARTESIAN_POINT ( 'NONE',  ( -21.92816239687475743, 42.46645089659918426, 13.50000000000000000 ) ) ;
#7837=CYLINDRICAL_SURFACE ( 'NONE', #15648, 0.2500000000000002220 ) ;
#7883=CIRCLE ( 'NONE', #4287, 0.2500000000000002220 ) ;
#7926=EDGE_LOOP ( 'NONE', ( #21914, #10474, #11199 ) ) ;
#7934=VERTEX_POINT ( 'NONE', #11292 ) ;
#7955=ORIENTED_EDGE ( 'NONE', *, *, #21703, .F. ) ;
#8009=DIRECTION ( 'NONE',  ( 1.000000000000000000, 0.000000000000000000, 0.000000000000000000 ) ) ;
#8014=TOROIDAL_SURFACE ( 'NONE', #12983, 2.076718556943726313, 0.2500000000000000000 ) ;
#8045=PRODUCT_DEFINITION_SHAPE ( 'NONE', 'NONE',  #7141 ) ;
#8048=DIRECTION ( 'NONE',  ( -1.000000000000000000, 0.000000000000000000, 0.000000000000000000 ) ) ;
#8091=ORIENTED_EDGE ( 'NONE', *, *, #1493, .F. ) ;
#8106=DIRECTION ( 'NONE',  ( -1.000000000000000000, 0.000000000000000000, 0.000000000000000000 ) ) ;
#8114=CIRCLE ( 'NONE', #21344, 2.076718556943725424 ) ;
#8116=DIRECTION ( 'NONE',  ( 0.2309407893632117181, -0.9729678061520313781, 0.000000000000000000 ) ) ;
#8120=DIRECTION ( 'NONE',  ( -0.9729678061520339316, -0.2309407893632008379, 1.418549243141864450E-14 ) ) ;
#8142=ORIENTED_EDGE ( 'NONE', *, *, #11521, .F. ) ;
#8169=AXIS2_PLACEMENT_3D ( 'NONE', #5567, #2297, #12245 ) ;
#8170=TOROIDAL_SURFACE ( 'NONE', #2787, 2.767785046117003489, 0.2500000000000000000 ) ;
#8204=FILL_AREA_STYLE ('',( #1356 ) ) ;
#8214=DIRECTION ( 'NONE',  ( -0.2309407893632007824, 0.9729678061520339316, 0.000000000000000000 ) ) ;
#8220=DIRECTION ( 'NONE',  ( -0.000000000000000000, -0.000000000000000000, -1.000000000000000000 ) ) ;
#8253=DIRECTION ( 'NONE',  ( 0.000000000000000000, 0.000000000000000000, 1.000000000000000000 ) ) ;
#8315=AXIS2_PLACEMENT_3D ( 'NONE', #21048, #5608, #17562 ) ;
#8337=CARTESIAN_POINT ( 'NONE',  ( -23.61959064016851073, 45.26242829375641463, 13.74999999999999822 ) ) ;
#8339=VERTEX_POINT ( 'NONE', #19681 ) ;
#8347=EDGE_CURVE ( 'NONE', #8339, #16466, #992, .T. ) ;
#8356=ORIENTED_EDGE ( 'NONE', *, *, #11805, .T. ) ;
#8469=EDGE_LOOP ( 'NONE', ( #20746, #5507, #5292, #5399 ) ) ;
#8478=DIRECTION ( 'NONE',  ( -1.000000000000000000, 0.000000000000000000, 0.000000000000000000 ) ) ;
#8491=ORIENTED_EDGE ( 'NONE', *, *, #3271, .T. ) ;
#8497=DIRECTION ( 'NONE',  ( -1.000000000000000000, 0.000000000000000000, 0.000000000000000000 ) ) ;
#8499=AXIS2_PLACEMENT_3D ( 'NONE', #1457, #18693, #3364 ) ;
#8500=EDGE_CURVE ( 'NONE', #5552, #573, #3443, .T. ) ;
#8517=CARTESIAN_POINT ( 'NONE',  ( -32.23382792203229741, 83.71979900898287497, 13.74999999999999822 ) ) ;
#8546=DIRECTION ( 'NONE',  ( 0.9969624470112576908, -0.07788375472025980961, -0.000000000000000000 ) ) ;
#8600=CARTESIAN_POINT ( 'NONE',  ( -21.71259690522456154, 45.22582864897715638, 13.50000000000000000 ) ) ;
#8602=CARTESIAN_POINT ( 'NONE',  ( -32.23382792203229741, 83.71979900898287497, 68.25000000000000000 ) ) ;
#8609=DIRECTION ( 'NONE',  ( -0.2309407893631976738, 0.9729678061520347088, 0.000000000000000000 ) ) ;
#8635=DIRECTION ( 'NONE',  ( 0.000000000000000000, -0.000000000000000000, -1.000000000000000000 ) ) ;
#8656=DIRECTION ( 'NONE',  ( 0.07788375472025979573, 0.9969624470112574688, 0.000000000000000000 ) ) ;
#8668=CARTESIAN_POINT ( 'NONE',  ( -31.01761816434227015, 84.00847499568689614, 68.25000000000000000 ) ) ;
#8674=CIRCLE ( 'NONE', #4739, 0.2500000000000002220 ) ;
#8677=DIRECTION ( 'NONE',  ( 0.000000000000000000, -0.000000000000000000, -1.000000000000000000 ) ) ;
#8706=ORIENTED_EDGE ( 'NONE', *, *, #14731, .F. ) ;
#8714=DIRECTION ( 'NONE',  ( -1.000000000000000000, 0.000000000000000000, 0.000000000000000000 ) ) ;
#8729=AXIS2_PLACEMENT_3D ( 'NONE', #8517, #15207, #5159 ) ;
#8755=DIRECTION ( 'NONE',  ( -1.000000000000000000, 0.000000000000000000, 0.000000000000000000 ) ) ;
#8768=ORIENTED_EDGE ( 'NONE', *, *, #17150, .T. ) ;
#8779=CYLINDRICAL_SURFACE ( 'NONE', #16017, 0.2500000000000001665 ) ;
#8807=DIRECTION ( 'NONE',  ( -1.000000000000000000, 0.000000000000000000, 0.000000000000000000 ) ) ;
#8814=DIRECTION ( 'NONE',  ( -1.000000000000000000, 0.000000000000000000, 0.000000000000000000 ) ) ;
#8820=VERTEX_POINT ( 'NONE', #7679 ) ;
#8866=DIRECTION ( 'NONE',  ( 0.000000000000000000, 0.000000000000000000, -1.000000000000000000 ) ) ;
#8882=CARTESIAN_POINT ( 'NONE',  ( -21.92816239687475743, 42.46645089659918426, 68.25000000000000000 ) ) ;
#8919=DIRECTION ( 'NONE',  ( 0.000000000000000000, 0.000000000000000000, 1.000000000000000000 ) ) ;
#8933=CARTESIAN_POINT ( 'NONE',  ( -32.47706987357030073, 83.66206381164208494, 13.74999999999999822 ) ) ;
#8955=CARTESIAN_POINT ( 'NONE',  ( -31.31859531322107060, 84.19398174988410233, 68.50000000000000000 ) ) ;
#8981=CYLINDRICAL_SURFACE ( 'NONE', #2130, 3.017785046117004377 ) ;
#8994=ORIENTED_EDGE ( 'NONE', *, *, #10465, .T. ) ;
#9022=PLANE ( 'NONE',  #16332 ) ;
#9034=ADVANCED_FACE ( 'NONE', ( #7003 ), #20538, .T. ) ;
#9056=CARTESIAN_POINT ( 'NONE',  ( -22.16013893094044462, 45.60883947780118319, 68.50000000000000000 ) ) ;
#9073=ORIENTED_EDGE ( 'NONE', *, *, #7716, .F. ) ;
#9101=DIRECTION ( 'NONE',  ( -0.9729678061520345977, -0.2309407893631976461, 0.000000000000000000 ) ) ;
#9127=AXIS2_PLACEMENT_3D ( 'NONE', #7333, #10894, #12560 ) ;
#9136=CARTESIAN_POINT ( 'NONE',  ( -21.92816239687475743, 42.46645089659918426, 13.74999999999999822 ) ) ;
#9142=SHAPE_REPRESENTATION ( 'Flap', ( #17493 ), #18569 ) ;
#9147=DIRECTION ( 'NONE',  ( 0.000000000000000000, 0.000000000000000000, 1.000000000000000000 ) ) ;
#9154=EDGE_CURVE ( 'NONE', #5908, #1345, #11411, .T. ) ;
#9156=ORIENTED_EDGE ( 'NONE', *, *, #20512, .F. ) ;
#9157=LINE ( 'NONE', #858, #19571 ) ;
#9178=ORIENTED_EDGE ( 'NONE', *, *, #16988, .T. ) ;
#9190=AXIS2_PLACEMENT_3D ( 'NONE', #18927, #8635, #13547 ) ;
#9220=AXIS2_PLACEMENT_3D ( 'NONE', #1654, #20241, #8497 ) ;
#9226=DIRECTION ( 'NONE',  ( 0.000000000000000000, 0.000000000000000000, 1.000000000000000000 ) ) ;
#9232=AXIS2_PLACEMENT_3D ( 'NONE', #2870, #3764, #8807 ) ;
#9233=CARTESIAN_POINT ( 'NONE',  ( -21.71259690522456154, 45.22582864897715638, 68.25000000000000000 ) ) ;
#9241=CIRCLE ( 'NONE', #16741, 3.017785046117004377 ) ;
#9245=VECTOR ( 'NONE', #22030, 1000.000000000000114 ) ;
#9296=VERTEX_POINT ( 'NONE', #205 ) ;
#9340=AXIS2_PLACEMENT_3D ( 'NONE', #17704, #7223, #587 ) ;
#9386=EDGE_CURVE ( 'NONE', #5113, #818, #10703, .T. ) ;
#9402=CARTESIAN_POINT ( 'NONE',  ( -21.87350007617872905, 45.48374084210715296, 13.75000000000000000 ) ) ;
#9405=ORIENTED_EDGE ( 'NONE', *, *, #15632, .F. ) ;
#9421=VERTEX_POINT ( 'NONE', #7173 ) ;
#9428=AXIS2_PLACEMENT_3D ( 'NONE', #19104, #4005, #10820 ) ;
#9444=ORIENTED_EDGE ( 'NONE', *, *, #21093, .T. ) ;
#9453=CARTESIAN_POINT ( 'NONE',  ( -31.26086011588027347, 83.95073979834609190, 68.25000000000000000 ) ) ;
#9457=CARTESIAN_POINT ( 'NONE',  ( -21.67365502786443088, 45.72430987248279166, 13.50000000000000000 ) ) ;
#9460=FACE_OUTER_BOUND ( 'NONE', #21192, .T. ) ;
#9462=CIRCLE ( 'NONE', #174, 0.2499999999999977796 ) ;
#9476=ORIENTED_EDGE ( 'NONE', *, *, #19586, .F. ) ;
#9497=VECTOR ( 'NONE', #12582, 1000.000000000000000 ) ;
#9509=LINE ( 'NONE', #9402, #21290 ) ;
#9556=DIRECTION ( 'NONE',  ( 0.9729678061520319332, 0.2309407893632090258, -0.000000000000000000 ) ) ;
#9566=AXIS2_PLACEMENT_3D ( 'NONE', #11227, #14805, #16384 ) ;
#9605=ORIENTED_EDGE ( 'NONE', *, *, #14065, .F. ) ;
#9617=DIRECTION ( 'NONE',  ( 0.000000000000000000, 0.000000000000000000, 1.000000000000000000 ) ) ;
#9627=PLANE ( 'NONE',  #7778 ) ;
#9690=ORIENTED_EDGE ( 'NONE', *, *, #20167, .F. ) ;
#9716=AXIS2_PLACEMENT_3D ( 'NONE', #6441, #8220, #8106 ) ;
#9728=VECTOR ( 'NONE', #9777, 1000.000000000000000 ) ;
#9746=AXIS2_PLACEMENT_3D ( 'NONE', #15783, #10768, #20844 ) ;
#9748=DIRECTION ( 'NONE',  ( 0.9729678061520478094, 0.2309407893631419961, 0.000000000000000000 ) ) ;
#9765=UNCERTAINTY_MEASURE_WITH_UNIT (LENGTH_MEASURE( 1.000000000000000082E-05 ), #9986, 'distance_accuracy_value', 'NONE');
#9767=CARTESIAN_POINT ( 'NONE',  ( 0.000000000000000000, 0.000000000000000000, 0.000000000000000000 ) ) ;
#9777=DIRECTION ( 'NONE',  ( 0.000000000000000000, -0.000000000000000000, -1.000000000000000000 ) ) ;
#9792=CARTESIAN_POINT ( 'NONE',  ( -19.16037735075775217, 42.46645089659918426, 68.50000000000000000 ) ) ;
#9806=EDGE_CURVE ( 'NONE', #3240, #5908, #20644, .T. ) ;
#9856=CARTESIAN_POINT ( 'NONE',  ( -23.37634868863050031, 45.32016349109721176, 68.25000000000000000 ) ) ;
#9860=DIRECTION ( 'NONE',  ( 0.000000000000000000, 0.000000000000000000, -1.000000000000000000 ) ) ;
#9866=ORIENTED_EDGE ( 'NONE', *, *, #12702, .T. ) ;
#9899=CIRCLE ( 'NONE', #4547, 0.2500000000000011657 ) ;
#9908=DIRECTION ( 'NONE',  ( -1.000000000000000000, 0.000000000000000000, 0.000000000000000000 ) ) ;
#9980=FACE_OUTER_BOUND ( 'NONE', #4884, .T. ) ;
#9986=( LENGTH_UNIT ( ) NAMED_UNIT ( * ) SI_UNIT ( .MILLI., .METRE. ) );
#9987=ORIENTED_EDGE ( 'NONE', *, *, #1725, .F. ) ;
#10013=APPLICATION_CONTEXT ( 'automotive_design' ) ;
#10077=CARTESIAN_POINT ( 'NONE',  ( -23.61959064016851073, 45.26242829375641463, 13.74999999999999822 ) ) ;
#10098=EDGE_CURVE ( 'NONE', #14287, #3240, #3536, .T. ) ;
#10104=FACE_OUTER_BOUND ( 'NONE', #21296, .T. ) ;
#10106=TOROIDAL_SURFACE ( 'NONE', #2186, 0.5000000000000000000, 0.2500000000000000000 ) ;
#10123=DIRECTION ( 'NONE',  ( 0.9729678061520313781, 0.2309407893632117181, 0.000000000000000000 ) ) ;
#10205=PRESENTATION_STYLE_ASSIGNMENT (( #3270 ) ) ;
#10213=FACE_OUTER_BOUND ( 'NONE', #21668, .T. ) ;
#10218=CIRCLE ( 'NONE', #14115, 0.2500000000000002220 ) ;
#10283=ADVANCED_FACE ( 'NONE', ( #18877 ), #6726, .T. ) ;
#10303=CARTESIAN_POINT ( 'NONE',  ( -19.85144383993102934, 42.46645089659918426, 13.74999999999999822 ) ) ;
#10317=DIRECTION ( 'NONE',  ( 0.2309407893632113573, -0.9729678061520313781, 0.000000000000000000 ) ) ;
#10331=EDGE_CURVE ( 'NONE', #1345, #10960, #21364, .T. ) ;
#10359=ORIENTED_EDGE ( 'NONE', *, *, #14138, .F. ) ;
#10397=EDGE_LOOP ( 'NONE', ( #14077, #6347, #3781 ) ) ;
#10409=ADVANCED_FACE ( 'NONE', ( #3758, #15601 ), #9022, .T. ) ;
#10425=ORIENTED_EDGE ( 'NONE', *, *, #20169, .F. ) ;
#10435=CARTESIAN_POINT ( 'NONE',  ( -31.01761816434227015, 84.00847499568689614, 13.75000000000000000 ) ) ;
#10451=DIRECTION ( 'NONE',  ( -0.9729678061520402599, -0.2309407893631745812, -0.000000000000000000 ) ) ;
#10452=EDGE_CURVE ( 'NONE', #15418, #5793, #12794, .T. ) ;
#10455=EDGE_CURVE ( 'NONE', #12289, #17196, #21010, .T. ) ;
#10456=CIRCLE ( 'NONE', #8315, 1.826718556943725202 ) ;
#10465=EDGE_CURVE ( 'NONE', #10522, #16645, #15274, .T. ) ;
#10471=FACE_OUTER_BOUND ( 'NONE', #18678, .T. ) ;
#10474=ORIENTED_EDGE ( 'NONE', *, *, #1887, .F. ) ;
#10501=DIRECTION ( 'NONE',  ( 0.000000000000000000, 0.000000000000000000, 1.000000000000000000 ) ) ;
#10502=DIRECTION ( 'NONE',  ( -1.000000000000000000, 0.000000000000000000, 0.000000000000000000 ) ) ;
#10504=EDGE_CURVE ( 'NONE', #14287, #21506, #13071, .T. ) ;
#10522=VERTEX_POINT ( 'NONE', #16148 ) ;
#10546=ORIENTED_EDGE ( 'NONE', *, *, #20532, .T. ) ;
#10595=ADVANCED_FACE ( 'NONE', ( #3295 ), #11998, .T. ) ;
#10597=DIRECTION ( 'NONE',  ( -1.000000000000000000, 0.000000000000000000, 0.000000000000000000 ) ) ;
#10605=ORIENTED_EDGE ( 'NONE', *, *, #15120, .F. ) ;
#10610=LINE ( 'NONE', #7046, #1379 ) ;
#10620=AXIS2_PLACEMENT_3D ( 'NONE', #13746, #7595, #10317 ) ;
#10646=AXIS2_PLACEMENT_3D ( 'NONE', #9453, #6458, #18181 ) ;
#10650=CARTESIAN_POINT ( 'NONE',  ( -24.00488095381848197, 42.46645089659918426, 68.50000000000000000 ) ) ;
#10660=CARTESIAN_POINT ( 'NONE',  ( -21.92816239687475743, 42.46645089659918426, 68.50000000000000000 ) ) ;
#10703=CIRCLE ( 'NONE', #687, 0.2500000000000002220 ) ;
#10712=ORIENTED_EDGE ( 'NONE', *, *, #3066, .T. ) ;
#10719=EDGE_CURVE ( 'NONE', #20520, #15862, #910, .T. ) ;
#10728=CARTESIAN_POINT ( 'NONE',  ( -21.92816239687475743, 42.46645089659918426, 13.74999999999999822 ) ) ;
#10749=AXIS2_PLACEMENT_3D ( 'NONE', #1479, #8546, #8656 ) ;
#10768=DIRECTION ( 'NONE',  ( 0.000000000000000000, 1.000000000000000000, -0.000000000000000000 ) ) ;
#10796=CARTESIAN_POINT ( 'NONE',  ( -18.91037735075775217, 42.46645089659918426, 68.50000000000000000 ) ) ;
#10820=DIRECTION ( 'NONE',  ( 0.000000000000000000, 0.000000000000000000, 1.000000000000000000 ) ) ;
#10832=ORIENTED_EDGE ( 'NONE', *, *, #10504, .T. ) ;
#10875=DIRECTION ( 'NONE',  ( -1.000000000000000000, 0.000000000000000000, 0.000000000000000000 ) ) ;
#10894=DIRECTION ( 'NONE',  ( 0.000000000000000000, 0.000000000000000000, 1.000000000000000000 ) ) ;
#10941=AXIS2_PLACEMENT_3D ( 'NONE', #15201, #21942, #20378 ) ;
#10951=ORIENTED_EDGE ( 'NONE', *, *, #21581, .T. ) ;
#10960=VERTEX_POINT ( 'NONE', #12258 ) ;
#10967=CARTESIAN_POINT ( 'NONE',  ( -21.92816239687475743, 42.46645089659918426, 68.50000000000000000 ) ) ;
#10973=AXIS2_PLACEMENT_3D ( 'NONE', #3405, #8677, #21992 ) ;
#11001=DIRECTION ( 'NONE',  ( -1.000000000000000000, 0.000000000000000000, 0.000000000000000000 ) ) ;
#11032=DIRECTION ( 'NONE',  ( 0.000000000000000000, 0.000000000000000000, 1.000000000000000000 ) ) ;
#11033=AXIS2_PLACEMENT_3D ( 'NONE', #12489, #10501, #20806 ) ;
#11108=ORIENTED_EDGE ( 'NONE', *, *, #21024, .F. ) ;
#11118=DIRECTION ( 'NONE',  ( 0.07788375472025979573, 0.9969624470112574688, 0.000000000000000000 ) ) ;
#11129=SPHERICAL_SURFACE ( 'NONE', #10646, 0.2500000000000000000 ) ;
#11134=CARTESIAN_POINT ( 'NONE',  ( -21.92816239687475743, 42.46645089659918426, 68.50000000000000000 ) ) ;
#11168=DIRECTION ( 'NONE',  ( -0.9729678061520314891, -0.2309407893632107189, 0.000000000000000000 ) ) ;
#11180=DIRECTION ( 'NONE',  ( -1.000000000000000000, 0.000000000000000000, 0.000000000000000000 ) ) ;
#11182=LINE ( 'NONE', #17261, #364 ) ;
#11199=ORIENTED_EDGE ( 'NONE', *, *, #7042, .T. ) ;
#11210=TOROIDAL_SURFACE ( 'NONE', #3724, 2.076718556943726313, 0.2500000000000000000 ) ;
#11221=ORIENTED_EDGE ( 'NONE', *, *, #7746, .T. ) ;
#11227=CARTESIAN_POINT ( 'NONE',  ( -32.23382792203229741, 83.71979900898287497, 68.25000000000000000 ) ) ;
#11270=DIRECTION ( 'NONE',  ( 0.000000000000000000, 0.000000000000000000, 1.000000000000000000 ) ) ;
#11292=CARTESIAN_POINT ( 'NONE',  ( -20.10144383993102934, 42.46645089659918426, 68.25000000000000000 ) ) ;
#11296=CARTESIAN_POINT ( 'NONE',  ( -21.69312596654449621, 45.47506926072997402, 68.25000000000000000 ) ) ;
#11312=ORIENTED_EDGE ( 'NONE', *, *, #5662, .F. ) ;
#11315=AXIS2_PLACEMENT_3D ( 'NONE', #3855, #14113, #2160 ) ;
#11342=ORIENTED_EDGE ( 'NONE', *, *, #1642, .F. ) ;
#11345=CARTESIAN_POINT ( 'NONE',  ( -31.26086011588027347, 83.95073979834609190, 68.25000000000000000 ) ) ;
#11356=CARTESIAN_POINT ( 'NONE',  ( -21.92816239687475743, 42.46645089659918426, 68.50000000000000000 ) ) ;
#11394=CIRCLE ( 'NONE', #19262, 3.017785046117004377 ) ;
#11403=DIRECTION ( 'NONE',  ( 0.000000000000000000, 1.000000000000000000, -0.000000000000000000 ) ) ;
#11411=CIRCLE ( 'NONE', #21426, 0.5000000000000004441 ) ;
#11416=DIRECTION ( 'NONE',  ( -0.000000000000000000, -0.000000000000000000, -1.000000000000000000 ) ) ;
#11435=ORIENTED_EDGE ( 'NONE', *, *, #21397, .T. ) ;
#11439=ADVANCED_FACE ( 'NONE', ( #21104 ), #7452, .T. ) ;
#11467=EDGE_CURVE ( 'NONE', #17196, #5035, #4078, .T. ) ;
#11471=DIRECTION ( 'NONE',  ( 0.000000000000000000, 0.000000000000000000, 1.000000000000000000 ) ) ;
#11477=ORIENTED_EDGE ( 'NONE', *, *, #4017, .F. ) ;
#11489=CARTESIAN_POINT ( 'NONE',  ( -32.23382792203229741, 83.71979900898287497, 68.25000000000000000 ) ) ;
#11502=DIRECTION ( 'NONE',  ( -1.000000000000000000, 0.000000000000000000, 0.000000000000000000 ) ) ;
#11521=EDGE_CURVE ( 'NONE', #14169, #20520, #18353, .T. ) ;
#11532=ORIENTED_EDGE ( 'NONE', *, *, #7716, .T. ) ;
#11536=ORIENTED_EDGE ( 'NONE', *, *, #8347, .F. ) ;
#11550=DIRECTION ( 'NONE',  ( -1.000000000000000000, 0.000000000000000000, 0.000000000000000000 ) ) ;
#11553=EDGE_LOOP ( 'NONE', ( #20036, #10712, #21798, #2958 ) ) ;
#11562=DIRECTION ( 'NONE',  ( -0.000000000000000000, -0.000000000000000000, -1.000000000000000000 ) ) ;
#11569=ADVANCED_FACE ( 'NONE', ( #20497 ), #15337, .F. ) ;
#11572=DIRECTION ( 'NONE',  ( -0.2309407893632139108, 0.9729678061520308230, 0.000000000000000000 ) ) ;
#11583=CARTESIAN_POINT ( 'NONE',  ( -21.92816239687475743, 42.46645089659918426, 68.25000000000000000 ) ) ;
#11598=DIRECTION ( 'NONE',  ( -1.000000000000000000, 0.000000000000000000, 0.000000000000000000 ) ) ;
#11613=ORIENTED_EDGE ( 'NONE', *, *, #14641, .F. ) ;
#11617=DIRECTION ( 'NONE',  ( -0.2309407893631451325, 0.9729678061520472543, 0.000000000000000000 ) ) ;
#11662=ADVANCED_FACE ( 'NONE', ( #11859 ), #3151, .T. ) ;
#11688=AXIS2_PLACEMENT_3D ( 'NONE', #4253, #11403, #16643 ) ;
#11694=EDGE_LOOP ( 'NONE', ( #3233, #15429, #10951, #39 ) ) ;
#11740=AXIS2_PLACEMENT_3D ( 'NONE', #15835, #19655, #21231 ) ;
#11773=DIRECTION ( 'NONE',  ( 0.000000000000000000, -0.000000000000000000, -1.000000000000000000 ) ) ;
#11775=DIRECTION ( 'NONE',  ( -1.000000000000000000, 0.000000000000000000, 0.000000000000000000 ) ) ;
#11785=DIRECTION ( 'NONE',  ( -1.000000000000000000, 0.000000000000000000, 0.000000000000000000 ) ) ;
#11794=FACE_OUTER_BOUND ( 'NONE', #2124, .T. ) ;
#11805=EDGE_CURVE ( 'NONE', #16312, #15418, #20656, .T. ) ;
#11815=AXIS2_PLACEMENT_3D ( 'NONE', #11489, #19673, #20122 ) ;
#11818=CARTESIAN_POINT ( 'NONE',  ( -32.48382792203229741, 83.71979900898287497, 13.74999999999999822 ) ) ;
#11834=CIRCLE ( 'NONE', #19658, 0.2499999999999977796 ) ;
#11844=EDGE_LOOP ( 'NONE', ( #17073, #4079 ) ) ;
#11850=EDGE_CURVE ( 'NONE', #6556, #1070, #18479, .T. ) ;
#11859=FACE_OUTER_BOUND ( 'NONE', #7594, .T. ) ;
#11920=ADVANCED_FACE ( 'NONE', ( #869, #18106 ), #9627, .F. ) ;
#11924=AXIS2_PLACEMENT_3D ( 'NONE', #7148, #13943, #10597 ) ;
#11939=ADVANCED_FACE ( 'NONE', ( #3344 ), #13141, .T. ) ;
#11943=DIRECTION ( 'NONE',  ( 0.000000000000000000, 0.000000000000000000, 1.000000000000000000 ) ) ;
#11951=ORIENTED_EDGE ( 'NONE', *, *, #5817, .F. ) ;
#11952=DIRECTION ( 'NONE',  ( -1.000000000000000000, 0.000000000000000000, 0.000000000000000000 ) ) ;
#11981=CARTESIAN_POINT ( 'NONE',  ( -21.92816239687475743, 42.46645089659918426, 68.50000000000000000 ) ) ;
#11994=ORIENTED_EDGE ( 'NONE', *, *, #1493, .T. ) ;
#11998=PLANE ( 'NONE',  #6311 ) ;
#12001=AXIS2_PLACEMENT_3D ( 'NONE', #21125, #11032, #2419 ) ;
#12009=FACE_OUTER_BOUND ( 'NONE', #2263, .T. ) ;
#12065=DIRECTION ( 'NONE',  ( -0.000000000000000000, -0.000000000000000000, -1.000000000000000000 ) ) ;
#12076=AXIS2_PLACEMENT_3D ( 'NONE', #7029, #16965, #8478 ) ;
#12095=DIRECTION ( 'NONE',  ( 1.000000000000000000, 0.000000000000000000, 0.000000000000000000 ) ) ;
#12118=CARTESIAN_POINT ( 'NONE',  ( -23.36078716634399655, 44.83461903493144973, 68.50000000000000000 ) ) ;
#12137=AXIS2_PLACEMENT_3D ( 'NONE', #4987, #13910, #4872 ) ;
#12145=DIRECTION ( 'NONE',  ( -1.000000000000000000, 0.000000000000000000, 0.000000000000000000 ) ) ;
#12155=ORIENTED_EDGE ( 'NONE', *, *, #15632, .T. ) ;
#12166=VERTEX_POINT ( 'NONE', #3786 ) ;
#12187=AXIS2_PLACEMENT_3D ( 'NONE', #13235, #19844, #20079 ) ;
#12190=ADVANCED_FACE ( 'NONE', ( #15743 ), #8170, .T. ) ;
#12192=VERTEX_POINT ( 'NONE', #17426 ) ;
#12198=DIRECTION ( 'NONE',  ( -0.000000000000000000, -0.000000000000000000, -1.000000000000000000 ) ) ;
#12224=CARTESIAN_POINT ( 'NONE',  ( -21.92816239687475743, 42.46645089659918426, 68.50000000000000000 ) ) ;
#12245=DIRECTION ( 'NONE',  ( 0.9729678061520314891, 0.2309407893632107189, 0.000000000000000000 ) ) ;
#12248=CARTESIAN_POINT ( 'NONE',  ( -32.47706987357030073, 83.66206381164208494, 68.50000000000000000 ) ) ;
#12254=ORIENTED_EDGE ( 'NONE', *, *, #13327, .T. ) ;
#12258=CARTESIAN_POINT ( 'NONE',  ( -21.91689697940243775, 45.66657467514198743, 68.25000000000000000 ) ) ;
#12265=ORIENTED_EDGE ( 'NONE', *, *, #12540, .T. ) ;
#12289=VERTEX_POINT ( 'NONE', #16281 ) ;
#12353=FACE_OUTER_BOUND ( 'NONE', #20499, .T. ) ;
#12374=FACE_OUTER_BOUND ( 'NONE', #6416, .T. ) ;
#12382=TOROIDAL_SURFACE ( 'NONE', #19541, 0.5000000000000000000, 0.2500000000000000000 ) ;
#12407=PRODUCT_CONTEXT ( 'NONE', #6897, 'mechanical' ) ;
#12439=AXIS2_PLACEMENT_3D ( 'NONE', #5934, #2566, #16303 ) ;
#12440=ADVANCED_FACE ( 'NONE', ( #10213 ), #6645, .F. ) ;
#12489=CARTESIAN_POINT ( 'NONE',  ( -21.92816239687475743, 42.46645089659918426, 13.74999999999999822 ) ) ;
#12499=DIRECTION ( 'NONE',  ( -0.9729678061520319332, -0.2309407893632090258, 0.000000000000000000 ) ) ;
#12528=CYLINDRICAL_SURFACE ( 'NONE', #13070, 3.017785046117004377 ) ;
#12529=CIRCLE ( 'NONE', #11815, 0.2500000000000002220 ) ;
#12540=EDGE_CURVE ( 'NONE', #5820, #12166, #9241, .T. ) ;
#12560=DIRECTION ( 'NONE',  ( -1.000000000000000000, 0.000000000000000000, 0.000000000000000000 ) ) ;
#12582=DIRECTION ( 'NONE',  ( -0.000000000000000000, -0.000000000000000000, 1.000000000000000000 ) ) ;
#12614=CARTESIAN_POINT ( 'NONE',  ( -23.49018890325625364, 45.04852366434393218, 13.74999999999999822 ) ) ;
#12615=ORIENTED_EDGE ( 'NONE', *, *, #7693, .F. ) ;
#12619=EDGE_CURVE ( 'NONE', #20520, #12192, #4246, .T. ) ;
#12630=ADVANCED_FACE ( 'NONE', ( #16531 ), #7837, .T. ) ;
#12642=EDGE_LOOP ( 'NONE', ( #19257, #2674, #3363, #9444 ) ) ;
#12661=EDGE_LOOP ( 'NONE', ( #2188, #218, #3513, #3907 ) ) ;
#12694=ORIENTED_EDGE ( 'NONE', *, *, #12540, .F. ) ;
#12702=EDGE_CURVE ( 'NONE', #1070, #14169, #11394, .T. ) ;
#12710=CARTESIAN_POINT ( 'NONE',  ( -23.36959064016851073, 45.26242829375641463, 13.74999999999999822 ) ) ;
#12711=DIRECTION ( 'NONE',  ( -0.9729678061520345977, -0.2309407893631976461, 0.000000000000000000 ) ) ;
#12720=DIRECTION ( 'NONE',  ( -6.751320378806396803E-15, -1.602473635475851075E-15, 1.000000000000000000 ) ) ;
#12770=EDGE_CURVE ( 'NONE', #5113, #18383, #13535, .T. ) ;
#12788=AXIS2_PLACEMENT_3D ( 'NONE', #19363, #5396, #541 ) ;
#12794=LINE ( 'NONE', #19751, #17413 ) ;
#12832=( GEOMETRIC_REPRESENTATION_CONTEXT ( 3 ) GLOBAL_UNCERTAINTY_ASSIGNED_CONTEXT ( ( #9765 ) ) GLOBAL_UNIT_ASSIGNED_CONTEXT ( ( #9986, #18591, #13661 ) ) REPRESENTATION_CONTEXT ( 'NONE', 'WORKASPACE' ) );
#12845=SHAPE_DEFINITION_REPRESENTATION ( #8045, #9142 ) ;
#12855=ORIENTED_EDGE ( 'NONE', *, *, #5375, .F. ) ;
#12861=CIRCLE ( 'NONE', #6472, 0.2499999999999977796 ) ;
#12894=LINE ( 'NONE', #14357, #7026 ) ;
#12905=EDGE_CURVE ( 'NONE', #5035, #2663, #3176, .T. ) ;
#12907=AXIS2_PLACEMENT_3D ( 'NONE', #1707, #1922, #11775 ) ;
#12930=ORIENTED_EDGE ( 'NONE', *, *, #16338, .T. ) ;
#12955=ORIENTED_EDGE ( 'NONE', *, *, #13020, .F. ) ;
#12983=AXIS2_PLACEMENT_3D ( 'NONE', #9136, #3772, #8714 ) ;
#12987=PRODUCT_DEFINITION_FORMATION_WITH_SPECIFIED_SOURCE ( 'ANY', '', #20392, .NOT_KNOWN. ) ;
#12990=VERTEX_POINT ( 'NONE', #949 ) ;
#12991=SURFACE_STYLE_FILL_AREA ( #21306 ) ;
#12992=ADVANCED_FACE ( 'NONE', ( #9460 ), #13148, .T. ) ;
#13020=EDGE_CURVE ( 'NONE', #16312, #2663, #14606, .T. ) ;
#13061=VECTOR ( 'NONE', #3977, 1000.000000000000000 ) ;
#13070=AXIS2_PLACEMENT_3D ( 'NONE', #15552, #17582, #4049 ) ;
#13071=CIRCLE ( 'NONE', #19159, 0.2500000000000002220 ) ;
#13082=ADVANCED_FACE ( 'NONE', ( #18192 ), #10106, .T. ) ;
#13107=ORIENTED_EDGE ( 'NONE', *, *, #20047, .T. ) ;
#13141=TOROIDAL_SURFACE ( 'NONE', #9220, 0.5000000000000000000, 0.2500000000000000000 ) ;
#13148=CYLINDRICAL_SURFACE ( 'NONE', #3266, 0.2499999999999985845 ) ;
#13153=CIRCLE ( 'NONE', #9232, 0.2500000000000002220 ) ;
#13181=CARTESIAN_POINT ( 'NONE',  ( -21.92816239687475743, 42.46645089659918426, 68.25000000000000000 ) ) ;
#13235=CARTESIAN_POINT ( 'NONE',  ( -32.23382792203229741, 83.71979900898287497, 13.75000000000000000 ) ) ;
#13293=CIRCLE ( 'NONE', #6535, 2.767785046117004377 ) ;
#13327=EDGE_CURVE ( 'NONE', #15418, #7129, #17205, .T. ) ;
#13347=AXIS2_PLACEMENT_3D ( 'NONE', #4540, #7806, #2422 ) ;
#13359=CARTESIAN_POINT ( 'NONE',  ( -10.73004499984425841, -2.546852060775805615, 68.25000000000000000 ) ) ;
#13387=EDGE_CURVE ( 'NONE', #7934, #6210, #16577, .T. ) ;
#13473=CYLINDRICAL_SURFACE ( 'NONE', #2353, 0.2500000000000001665 ) ;
#13475=CARTESIAN_POINT ( 'NONE',  ( -19.85144383993102934, 42.46645089659918426, 68.25000000000000000 ) ) ;
#13499=DIRECTION ( 'NONE',  ( 0.000000000000000000, 0.000000000000000000, 1.000000000000000000 ) ) ;
#13505=AXIS2_PLACEMENT_3D ( 'NONE', #16529, #4451, #12711 ) ;
#13520=EDGE_CURVE ( 'NONE', #818, #2269, #13767, .T. ) ;
#13535=CIRCLE ( 'NONE', #3906, 2.076718556943725424 ) ;
#13547=DIRECTION ( 'NONE',  ( 1.000000000000000000, 0.000000000000000000, 0.000000000000000000 ) ) ;
#13575=ORIENTED_EDGE ( 'NONE', *, *, #20169, .T. ) ;
#13584=VERTEX_POINT ( 'NONE', #3506 ) ;
#13623=FACE_OUTER_BOUND ( 'NONE', #12661, .T. ) ;
#13626=LINE ( 'NONE', #16634, #18043 ) ;
#13647=CARTESIAN_POINT ( 'NONE',  ( -24.00488095381848197, 42.46645089659918426, 13.49999999999999822 ) ) ;
#13661=( NAMED_UNIT ( * ) SI_UNIT ( $, .STERADIAN. ) SOLID_ANGLE_UNIT ( ) );
#13662=ORIENTED_EDGE ( 'NONE', *, *, #18692, .T. ) ;
#13665=CYLINDRICAL_SURFACE ( 'NONE', #2346, 0.2500000000000002220 ) ;
#13682=CARTESIAN_POINT ( 'NONE',  ( -23.36078716634399655, 44.83461903493144973, 68.25000000000000000 ) ) ;
#13699=ORIENTED_EDGE ( 'NONE', *, *, #5765, .F. ) ;
#13706=ORIENTED_EDGE ( 'NONE', *, *, #13387, .T. ) ;
#13736=DIRECTION ( 'NONE',  ( 1.000000000000000000, 0.000000000000000000, 0.000000000000000000 ) ) ;
#13746=CARTESIAN_POINT ( 'NONE',  ( -11.94625475753432120, -2.835528047479821900, 68.50000000000000000 ) ) ;
#13765=( LENGTH_UNIT ( ) NAMED_UNIT ( * ) SI_UNIT ( .MILLI., .METRE. ) );
#13767=LINE ( 'NONE', #18605, #16492 ) ;
#13788=DIRECTION ( 'NONE',  ( -1.000000000000000000, 0.000000000000000000, 0.000000000000000000 ) ) ;
#13789=DIRECTION ( 'NONE',  ( 0.9729678061520314891, 0.2309407893632107189, 0.000000000000000000 ) ) ;
#13804=AXIS2_PLACEMENT_3D ( 'NONE', #13475, #15148, #17168 ) ;
#13814=DIRECTION ( 'NONE',  ( 0.000000000000000000, 0.000000000000000000, 1.000000000000000000 ) ) ;
#13817=CARTESIAN_POINT ( 'NONE',  ( -21.92816239687475743, 42.46645089659918426, 13.50000000000000000 ) ) ;
#13819=DIRECTION ( 'NONE',  ( 1.000000000000000000, 0.000000000000000000, 0.000000000000000000 ) ) ;
#13831=CARTESIAN_POINT ( 'NONE',  ( -21.92816239687475743, 42.46645089659918426, 13.74999999999999822 ) ) ;
#13910=DIRECTION ( 'NONE',  ( 0.000000000000000000, 0.000000000000000000, 1.000000000000000000 ) ) ;
#13943=DIRECTION ( 'NONE',  ( -0.000000000000000000, -0.000000000000000000, -1.000000000000000000 ) ) ;
#14016=DIRECTION ( 'NONE',  ( -0.2309407893632117181, 0.9729678061520313781, 0.000000000000000000 ) ) ;
#14018=SPHERICAL_SURFACE ( 'NONE', #3230, 0.2500000000000000000 ) ;
#14061=ORIENTED_EDGE ( 'NONE', *, *, #14541, .T. ) ;
#14065=EDGE_CURVE ( 'NONE', #2269, #6210, #10456, .T. ) ;
#14077=ORIENTED_EDGE ( 'NONE', *, *, #17150, .F. ) ;
#14092=DIRECTION ( 'NONE',  ( 0.5176069476490314791, -0.8556185176499236933, 0.000000000000000000 ) ) ;
#14113=DIRECTION ( 'NONE',  ( 0.000000000000000000, 0.000000000000000000, 1.000000000000000000 ) ) ;
#14115=AXIS2_PLACEMENT_3D ( 'NONE', #2675, #13499, #5012 ) ;
#14138=EDGE_CURVE ( 'NONE', #2663, #12289, #2120, .T. ) ;
#14139=AXIS2_PLACEMENT_3D ( 'NONE', #19151, #7300, #14092 ) ;
#14141=DIRECTION ( 'NONE',  ( -1.000000000000000000, 0.000000000000000000, 0.000000000000000000 ) ) ;
#14169=VERTEX_POINT ( 'NONE', #12614 ) ;
#14243=CARTESIAN_POINT ( 'NONE',  ( -21.67365502786443088, 45.72430987248279166, 68.50000000000000000 ) ) ;
#14257=ORIENTED_EDGE ( 'NONE', *, *, #10455, .T. ) ;
#14271=FACE_OUTER_BOUND ( 'NONE', #413, .T. ) ;
#14287=VERTEX_POINT ( 'NONE', #7010 ) ;
#14333=CARTESIAN_POINT ( 'NONE',  ( -10.48680304830625154, -2.489116863435002713, 68.25000000000000000 ) ) ;
#14336=CIRCLE ( 'NONE', #9716, 2.767785046117004377 ) ;
#14342=EDGE_LOOP ( 'NONE', ( #3166, #7481, #11532, #4062 ) ) ;
#14357=CARTESIAN_POINT ( 'NONE',  ( -23.37634868863050386, 45.32016349109721176, 13.49999999999999822 ) ) ;
#14411=ORIENTED_EDGE ( 'NONE', *, *, #2648, .F. ) ;
#14454=CARTESIAN_POINT ( 'NONE',  ( -20.53081511603577525, 86.49759185912193971, 68.50000000000000000 ) ) ;
#14517=CARTESIAN_POINT ( 'NONE',  ( -32.23382792203229741, 83.71979900898287497, 13.75000000000000000 ) ) ;
#14537=CIRCLE ( 'NONE', #20278, 0.2500000000000002220 ) ;
#14541=EDGE_CURVE ( 'NONE', #14287, #12166, #5990, .T. ) ;
#14560=CARTESIAN_POINT ( 'NONE',  ( -19.16037735075775217, 42.46645089659918426, 13.50000000000000000 ) ) ;
#14569=ORIENTED_EDGE ( 'NONE', *, *, #20047, .F. ) ;
#14606=LINE ( 'NONE', #1069, #17947 ) ;
#14641=EDGE_CURVE ( 'NONE', #799, #15862, #14336, .T. ) ;
#14681=ORIENTED_EDGE ( 'NONE', *, *, #18303, .F. ) ;
#14682=FILL_AREA_STYLE_COLOUR ( '', #3951 ) ;
#14700=DIRECTION ( 'NONE',  ( -1.000000000000000000, 0.000000000000000000, 0.000000000000000000 ) ) ;
#14731=EDGE_CURVE ( 'NONE', #12166, #1070, #6514, .T. ) ;
#14753=CYLINDRICAL_SURFACE ( 'NONE', #12439, 0.2500000000000002220 ) ;
#14773=EDGE_CURVE ( 'NONE', #21506, #799, #7590, .T. ) ;
#14775=DIRECTION ( 'NONE',  ( 0.000000000000000000, 0.000000000000000000, 1.000000000000000000 ) ) ;
#14805=DIRECTION ( 'NONE',  ( -0.9729678061520339316, -0.2309407893632008379, 0.000000000000000000 ) ) ;
#14842=CARTESIAN_POINT ( 'NONE',  ( -24.69594744299175915, 42.46645089659918426, 68.50000000000000000 ) ) ;
#14849=AXIS2_PLACEMENT_3D ( 'NONE', #17019, #5068, #4418 ) ;
#14889=ORIENTED_EDGE ( 'NONE', *, *, #20011, .F. ) ;
#14891=UNCERTAINTY_MEASURE_WITH_UNIT (LENGTH_MEASURE( 1.000000000000000082E-05 ), #19957, 'distance_accuracy_value', 'NONE');
#14920=DIRECTION ( 'NONE',  ( 0.5176069476490314791, -0.8556185176499236933, 0.000000000000000000 ) ) ;
#14932=ORIENTED_EDGE ( 'NONE', *, *, #20512, .T. ) ;
#14949=CARTESIAN_POINT ( 'NONE',  ( -32.29156311937309454, 83.96304096052088539, 68.25000000000000000 ) ) ;
#14952=AXIS2_PLACEMENT_3D ( 'NONE', #11981, #21865, #5180 ) ;
#14979=AXIS2_PLACEMENT_3D ( 'NONE', #16084, #19686, #11168 ) ;
#15005=CARTESIAN_POINT ( 'NONE',  ( -23.49018890325625364, 45.04852366434393218, 68.50000000000000000 ) ) ;
#15016=( NAMED_UNIT ( * ) SI_UNIT ( $, .STERADIAN. ) SOLID_ANGLE_UNIT ( ) );
#15084=ORIENTED_EDGE ( 'NONE', *, *, #21884, .T. ) ;
#15085=EDGE_CURVE ( 'NONE', #6210, #1592, #8674, .T. ) ;
#15095=EDGE_LOOP ( 'NONE', ( #20552, #21897, #16899, #13575 ) ) ;
#15120=EDGE_CURVE ( 'NONE', #12990, #10522, #17767, .T. ) ;
#15147=ORIENTED_EDGE ( 'NONE', *, *, #13327, .F. ) ;
#15148=DIRECTION ( 'NONE',  ( -1.224646799147353207E-16, -1.000000000000000000, 0.000000000000000000 ) ) ;
#15168=VERTEX_POINT ( 'NONE', #12710 ) ;
#15175=DIRECTION ( 'NONE',  ( 0.000000000000000000, 0.000000000000000000, 1.000000000000000000 ) ) ;
#15180=CARTESIAN_POINT ( 'NONE',  ( -11.70301280599631610, -2.777792850139019443, 13.50000000000000000 ) ) ;
#15201=CARTESIAN_POINT ( 'NONE',  ( -23.13310673709249343, 45.37789868843801599, 68.25000000000000000 ) ) ;
#15205=AXIS2_PLACEMENT_3D ( 'NONE', #19529, #4001, #16157 ) ;
#15207=DIRECTION ( 'NONE',  ( -0.2309407893632007824, 0.9729678061520339316, 6.042045757235441622E-14 ) ) ;
#15274=CIRCLE ( 'NONE', #9566, 0.2499999999999977796 ) ;
#15277=EDGE_LOOP ( 'NONE', ( #17892, #3926, #10546, #12265 ) ) ;
#15337=CYLINDRICAL_SURFACE ( 'NONE', #9190, 0.2500000000000002220 ) ;
#15355=MECHANICAL_DESIGN_GEOMETRIC_PRESENTATION_REPRESENTATION('',(#338),#12832);
#15372=CIRCLE ( 'NONE', #714, 1.826718556943725202 ) ;
#15382=DIRECTION ( 'NONE',  ( 0.000000000000000000, -0.000000000000000000, -1.000000000000000000 ) ) ;
#15418=VERTEX_POINT ( 'NONE', #11818 ) ;
#15429=ORIENTED_EDGE ( 'NONE', *, *, #20167, .T. ) ;
#15477=FACE_OUTER_BOUND ( 'NONE', #14342, .T. ) ;
#15502=CARTESIAN_POINT ( 'NONE',  ( -19.16037735075775217, 42.46645089659918426, 13.74999999999999822 ) ) ;
#15506=ORIENTED_EDGE ( 'NONE', *, *, #4858, .T. ) ;
#15519=DIRECTION ( 'NONE',  ( -1.000000000000000000, 0.000000000000000000, 0.000000000000000000 ) ) ;
#15552=CARTESIAN_POINT ( 'NONE',  ( -21.92816239687475743, 42.46645089659918426, 68.50000000000000000 ) ) ;
#15563=VECTOR ( 'NONE', #9556, 1000.000000000000114 ) ;
#15593=CIRCLE ( 'NONE', #20963, 0.5000000000000004441 ) ;
#15601=FACE_OUTER_BOUND ( 'NONE', #21807, .T. ) ;
#15604=ADVANCED_FACE ( 'NONE', ( #14271 ), #17527, .T. ) ;
#15632=EDGE_CURVE ( 'NONE', #7129, #9421, #5797, .T. ) ;
#15648=AXIS2_PLACEMENT_3D ( 'NONE', #21924, #6495, #11598 ) ;
#15681=ADVANCED_FACE ( 'NONE', ( #16595 ), #16498, .F. ) ;
#15743=FACE_OUTER_BOUND ( 'NONE', #7027, .T. ) ;
#15747=ORIENTED_EDGE ( 'NONE', *, *, #10098, .F. ) ;
#15764=ORIENTED_EDGE ( 'NONE', *, *, #8500, .T. ) ;
#15783=CARTESIAN_POINT ( 'NONE',  ( -24.69594744299175915, 42.46645089659918426, 68.25000000000000000 ) ) ;
#15788=DIRECTION ( 'NONE',  ( 1.000000000000000000, 0.000000000000000000, 0.000000000000000000 ) ) ;
#15818=CARTESIAN_POINT ( 'NONE',  ( -21.92816239687475743, 42.46645089659918426, 68.25000000000000000 ) ) ;
#15825=ADVANCED_FACE ( 'NONE', ( #6999 ), #13473, .T. ) ;
#15835=CARTESIAN_POINT ( 'NONE',  ( -31.26086011588028057, 83.95073979834609190, 13.75000000000000000 ) ) ;
#15862=VERTEX_POINT ( 'NONE', #12118 ) ;
#15890=AXIS2_PLACEMENT_3D ( 'NONE', #3005, #11270, #8048 ) ;
#16017=AXIS2_PLACEMENT_3D ( 'NONE', #18628, #16941, #22121 ) ;
#16031=EDGE_CURVE ( 'NONE', #8820, #5552, #7219, .T. ) ;
#16071=VERTEX_POINT ( 'NONE', #5978 ) ;
#16083=DIRECTION ( 'NONE',  ( 0.000000000000000000, 1.000000000000000000, -0.000000000000000000 ) ) ;
#16084=CARTESIAN_POINT ( 'NONE',  ( -10.73004499984425841, -2.546852060775806059, 13.75000000000000000 ) ) ;
#16113=DIRECTION ( 'NONE',  ( 0.2309407893632113573, -0.9729678061520313781, -0.000000000000000000 ) ) ;
#16145=ORIENTED_EDGE ( 'NONE', *, *, #14065, .T. ) ;
#16148=CARTESIAN_POINT ( 'NONE',  ( -32.23382792203229741, 83.71979900898287497, 68.50000000000000000 ) ) ;
#16157=DIRECTION ( 'NONE',  ( -1.000000000000000000, 0.000000000000000000, 0.000000000000000000 ) ) ;
#16203=ORIENTED_EDGE ( 'NONE', *, *, #20183, .F. ) ;
#16205=ORIENTED_EDGE ( 'NONE', *, *, #15085, .T. ) ;
#16226=DIRECTION ( 'NONE',  ( 1.000000000000000000, 0.000000000000000000, 0.000000000000000000 ) ) ;
#16230=DIRECTION ( 'NONE',  ( 0.000000000000000000, 1.000000000000000000, -0.000000000000000000 ) ) ;
#16247=DIRECTION ( 'NONE',  ( 0.9969624470112576908, -0.07788375472025980961, -0.000000000000000000 ) ) ;
#16281=CARTESIAN_POINT ( 'NONE',  ( -31.31859531322107060, 84.19398174988410233, 68.25000000000000000 ) ) ;
#16303=DIRECTION ( 'NONE',  ( 1.000000000000000000, 0.000000000000000000, 0.000000000000000000 ) ) ;
#16312=VERTEX_POINT ( 'NONE', #19483 ) ;
#16326=CLOSED_SHELL ( 'NONE', ( #19614, #3944, #12190, #1111, #10283, #3715, #3749, #2681, #20288, #12630, #12440, #19540, #9034, #22077, #16501, #11662, #10595, #15681, #10409, #11920, #11439, #4608, #17688, #12992, #2491, #19092, #18756, #760, #4996, #18897, #13082, #19088, #15604, #15825, #7529, #19242, #3634, #1568, #11939, #11569, #1727, #2041 ) ) ;
#16332=AXIS2_PLACEMENT_3D ( 'NONE', #491, #13814, #14141 ) ;
#16338=EDGE_CURVE ( 'NONE', #9421, #20875, #19604, .T. ) ;
#16346=EDGE_CURVE ( 'NONE', #22161, #18590, #3096, .T. ) ;
#16372=DIRECTION ( 'NONE',  ( -0.000000000000000000, -0.000000000000000000, -1.000000000000000000 ) ) ;
#16384=DIRECTION ( 'NONE',  ( -0.2309407893632007824, 0.9729678061520339316, 0.000000000000000000 ) ) ;
#16395=DIRECTION ( 'NONE',  ( 0.000000000000000000, 0.000000000000000000, 1.000000000000000000 ) ) ;
#16438=CARTESIAN_POINT ( 'NONE',  ( 0.000000000000000000, 0.000000000000000000, 13.50000000000000000 ) ) ;
#16466=VERTEX_POINT ( 'NONE', #20498 ) ;
#16491=DIRECTION ( 'NONE',  ( -0.000000000000000000, -0.000000000000000000, -1.000000000000000000 ) ) ;
#16492=VECTOR ( 'NONE', #11773, 1000.000000000000000 ) ;
#16495=CARTESIAN_POINT ( 'NONE',  ( -32.23382792203230451, 83.71979900898288918, 13.50000000000000000 ) ) ;
#16498=CYLINDRICAL_SURFACE ( 'NONE', #20940, 1.826718556943725202 ) ;
#16501=ADVANCED_FACE ( 'NONE', ( #9980 ), #19667, .F. ) ;
#16512=ORIENTED_EDGE ( 'NONE', *, *, #13387, .F. ) ;
#16529=CARTESIAN_POINT ( 'NONE',  ( -23.13310673709249343, 45.37789868843801599, 13.75000000000000000 ) ) ;
#16531=FACE_OUTER_BOUND ( 'NONE', #3730, .T. ) ;
#16577=LINE ( 'NONE', #6439, #9728 ) ;
#16581=ORIENTED_EDGE ( 'NONE', *, *, #2410, .F. ) ;
#16595=FACE_OUTER_BOUND ( 'NONE', #17266, .T. ) ;
#16634=CARTESIAN_POINT ( 'NONE',  ( -32.29156311937309454, 83.96304096052088539, 13.49999999999999822 ) ) ;
#16643=DIRECTION ( 'NONE',  ( 0.000000000000000000, 0.000000000000000000, 1.000000000000000000 ) ) ;
#16645=VERTEX_POINT ( 'NONE', #14949 ) ;
#16671=ORIENTED_EDGE ( 'NONE', *, *, #14773, .T. ) ;
#16691=AXIS2_PLACEMENT_3D ( 'NONE', #15818, #485, #7339 ) ;
#16741=AXIS2_PLACEMENT_3D ( 'NONE', #20623, #12198, #8755 ) ;
#16757=CARTESIAN_POINT ( 'NONE',  ( -31.26086011588028057, 83.95073979834609190, 68.25000000000000000 ) ) ;
#16791=AXIS2_PLACEMENT_3D ( 'NONE', #584, #7325, #9101 ) ;
#16899=ORIENTED_EDGE ( 'NONE', *, *, #19837, .F. ) ;
#16911=PRODUCT_DEFINITION_CONTEXT ( 'detailed design', #10013, 'design' ) ;
#16924=ORIENTED_EDGE ( 'NONE', *, *, #14138, .T. ) ;
#16936=DIRECTION ( 'NONE',  ( 0.000000000000000000, 0.000000000000000000, 1.000000000000000000 ) ) ;
#16941=DIRECTION ( 'NONE',  ( 0.2309407893632113573, -0.9729678061520313781, 0.000000000000000000 ) ) ;
#16952=ORIENTED_EDGE ( 'NONE', *, *, #11850, .T. ) ;
#16965=DIRECTION ( 'NONE',  ( 0.000000000000000000, -1.000000000000000000, 0.000000000000000000 ) ) ;
#16988=EDGE_CURVE ( 'NONE', #12192, #14287, #17074, .T. ) ;
#17009=ORIENTED_EDGE ( 'NONE', *, *, #13520, .T. ) ;
#17019=CARTESIAN_POINT ( 'NONE',  ( -23.61959064016851073, 45.26242829375641463, 13.74999999999999822 ) ) ;
#17027=CARTESIAN_POINT ( 'NONE',  ( -32.23382792203230451, 83.71979900898288918, 13.75000000000000000 ) ) ;
#17073=ORIENTED_EDGE ( 'NONE', *, *, #21093, .F. ) ;
#17074=CIRCLE ( 'NONE', #16691, 3.017785046117004377 ) ;
#17104=TOROIDAL_SURFACE ( 'NONE', #20981, 0.5000000000000000000, 0.2500000000000000000 ) ;
#17109=EDGE_LOOP ( 'NONE', ( #5477, #14889 ) ) ;
#17111=ORIENTED_EDGE ( 'NONE', *, *, #20301, .F. ) ;
#17140=CARTESIAN_POINT ( 'NONE',  ( -31.26086011588027347, 83.95073979834609190, 68.50000000000000000 ) ) ;
#17150=EDGE_CURVE ( 'NONE', #9296, #12289, #1328, .T. ) ;
#17168=DIRECTION ( 'NONE',  ( 1.000000000000000000, 0.000000000000000000, 0.000000000000000000 ) ) ;
#17196=VERTEX_POINT ( 'NONE', #8668 ) ;
#17205=CIRCLE ( 'NONE', #12187, 0.2500000000000002220 ) ;
#17261=CARTESIAN_POINT ( 'NONE',  ( -10.73004499984425664, -2.546852060775805615, 68.50000000000000000 ) ) ;
#17266=EDGE_LOOP ( 'NONE', ( #17641, #4064, #13706, #9605 ) ) ;
#17267=DIRECTION ( 'NONE',  ( -0.000000000000000000, -0.000000000000000000, 1.000000000000000000 ) ) ;
#17323=ORIENTED_EDGE ( 'NONE', *, *, #11850, .F. ) ;
#17341=CIRCLE ( 'NONE', #2351, 1.826718556943725202 ) ;
#17388=EDGE_LOOP ( 'NONE', ( #11536, #14411, #3652, #3392, #14681 ) ) ;
#17397=CARTESIAN_POINT ( 'NONE',  ( -22.16013893094044462, 45.60883947780118319, 68.25000000000000000 ) ) ;
#17413=VECTOR ( 'NONE', #824, 1000.000000000000000 ) ;
#17426=CARTESIAN_POINT ( 'NONE',  ( -24.94594744299175915, 42.46645089659918426, 68.25000000000000000 ) ) ;
#17459=EDGE_LOOP ( 'NONE', ( #9987, #8491, #15147 ) ) ;
#17484=DIRECTION ( 'NONE',  ( -1.000000000000000000, 0.000000000000000000, 0.000000000000000000 ) ) ;
#17493=AXIS2_PLACEMENT_3D ( 'NONE', #9767, #1237, #16226 ) ;
#17502=LINE ( 'NONE', #156, #13061 ) ;
#17527=SPHERICAL_SURFACE ( 'NONE', #15205, 0.2500000000000000000 ) ;
#17562=DIRECTION ( 'NONE',  ( -1.000000000000000000, 0.000000000000000000, 0.000000000000000000 ) ) ;
#17567=CIRCLE ( 'NONE', #9340, 0.5000000000000004441 ) ;
#17575=CARTESIAN_POINT ( 'NONE',  ( -23.75488095381848197, 42.46645089659918426, 13.74999999999999822 ) ) ;
#17576=EDGE_LOOP ( 'NONE', ( #21342, #5168, #10425, #11312 ) ) ;
#17582=DIRECTION ( 'NONE',  ( 0.000000000000000000, -0.000000000000000000, -1.000000000000000000 ) ) ;
#17619=DIRECTION ( 'NONE',  ( -0.9729678061520345977, -0.2309407893631976461, 0.000000000000000000 ) ) ;
#17641=ORIENTED_EDGE ( 'NONE', *, *, #13520, .F. ) ;
#17688=ADVANCED_FACE ( 'NONE', ( #3704 ), #18931, .T. ) ;
#17698=CARTESIAN_POINT ( 'NONE',  ( -31.31859531322107770, 84.19398174988410233, 13.50000000000000000 ) ) ;
#17704=CARTESIAN_POINT ( 'NONE',  ( -23.61959064016851073, 45.26242829375641463, 13.50000000000000000 ) ) ;
#17757=AXIS2_PLACEMENT_3D ( 'NONE', #7762, #16230, #6202 ) ;
#17767=LINE ( 'NONE', #2555, #20814 ) ;
#17780=AXIS2_PLACEMENT_3D ( 'NONE', #17397, #5562, #17619 ) ;
#17792=AXIS2_PLACEMENT_3D ( 'NONE', #15502, #171, #13819 ) ;
#17817=DIRECTION ( 'NONE',  ( -1.000000000000000000, 0.000000000000000000, 0.000000000000000000 ) ) ;
#17868=ORIENTED_EDGE ( 'NONE', *, *, #5817, .T. ) ;
#17892=ORIENTED_EDGE ( 'NONE', *, *, #18692, .F. ) ;
#17922=TOROIDAL_SURFACE ( 'NONE', #18284, 2.767785046117003489, 0.2500000000000000000 ) ;
#17938=DIRECTION ( 'NONE',  ( 0.000000000000000000, -0.000000000000000000, -1.000000000000000000 ) ) ;
#17947=VECTOR ( 'NONE', #18398, 1000.000000000000114 ) ;
#18010=DIRECTION ( 'NONE',  ( -1.000000000000000000, 0.000000000000000000, 0.000000000000000000 ) ) ;
#18029=EDGE_LOOP ( 'NONE', ( #9156, #937, #11435, #15764 ) ) ;
#18043=VECTOR ( 'NONE', #94, 1000.000000000000000 ) ;
#18093=CIRCLE ( 'NONE', #10941, 0.2500000000000011657 ) ;
#18104=ORIENTED_EDGE ( 'NONE', *, *, #16346, .F. ) ;
#18106=FACE_OUTER_BOUND ( 'NONE', #18328, .T. ) ;
#18131=AXIS2_PLACEMENT_3D ( 'NONE', #11583, #8253, #20215 ) ;
#18181=DIRECTION ( 'NONE',  ( -1.000000000000000000, 0.000000000000000000, 0.000000000000000000 ) ) ;
#18192=FACE_OUTER_BOUND ( 'NONE', #7514, .T. ) ;
#18252=EDGE_LOOP ( 'NONE', ( #11108, #19994, #8994 ) ) ;
#18272=VECTOR ( 'NONE', #17938, 1000.000000000000000 ) ;
#18284=AXIS2_PLACEMENT_3D ( 'NONE', #7353, #8919, #12145 ) ;
#18289=ORIENTED_EDGE ( 'NONE', *, *, #12905, .F. ) ;
#18303=EDGE_CURVE ( 'NONE', #16466, #15168, #14537, .T. ) ;
#18328=EDGE_LOOP ( 'NONE', ( #2162, #5448, #13107, #18104, #11951, #8091, #3346, #11342 ) ) ;
#18353=LINE ( 'NONE', #15005, #5976 ) ;
#18383=VERTEX_POINT ( 'NONE', #7271 ) ;
#18398=DIRECTION ( 'NONE',  ( 0.9729678061520319332, 0.2309407893632090258, -0.000000000000000000 ) ) ;
#18443=EDGE_CURVE ( 'NONE', #12289, #16645, #9157, .T. ) ;
#18450=AXIS2_PLACEMENT_3D ( 'NONE', #4928, #11617, #9748 ) ;
#18465=AXIS2_PLACEMENT_3D ( 'NONE', #7836, #1097, #21596 ) ;
#18477=VERTEX_POINT ( 'NONE', #5821 ) ;
#18479=CIRCLE ( 'NONE', #11688, 0.2500000000000002220 ) ;
#18512=ORIENTED_EDGE ( 'NONE', *, *, #10452, .F. ) ;
#18569=( GEOMETRIC_REPRESENTATION_CONTEXT ( 3 ) GLOBAL_UNCERTAINTY_ASSIGNED_CONTEXT ( ( #14891 ) ) GLOBAL_UNIT_ASSIGNED_CONTEXT ( ( #19957, #2939, #15016 ) ) REPRESENTATION_CONTEXT ( 'NONE', 'WORKASPACE' ) );
#18590=VERTEX_POINT ( 'NONE', #8600 ) ;
#18591=( NAMED_UNIT ( * ) PLANE_ANGLE_UNIT ( ) SI_UNIT ( $, .RADIAN. ) );
#18605=CARTESIAN_POINT ( 'NONE',  ( -23.75488095381848197, 42.46645089659918426, 68.50000000000000000 ) ) ;
#18628=CARTESIAN_POINT ( 'NONE',  ( -11.70301280599631433, -2.777792850139018999, 68.25000000000000000 ) ) ;
#18631=ORIENTED_EDGE ( 'NONE', *, *, #11467, .T. ) ;
#18647=DIRECTION ( 'NONE',  ( -0.000000000000000000, -0.000000000000000000, -1.000000000000000000 ) ) ;
#18662=DIRECTION ( 'NONE',  ( 0.2309407893632113573, -0.9729678061520313781, -0.000000000000000000 ) ) ;
#18678=EDGE_LOOP ( 'NONE', ( #7663, #3267, #115, #185 ) ) ;
#18692=EDGE_CURVE ( 'NONE', #22161, #12166, #1709, .T. ) ;
#18693=DIRECTION ( 'NONE',  ( -0.2309407893632090258, 0.9729678061520319332, 0.000000000000000000 ) ) ;
#18702=ORIENTED_EDGE ( 'NONE', *, *, #7042, .F. ) ;
#18712=LINE ( 'NONE', #21973, #21561 ) ;
#18744=FACE_OUTER_BOUND ( 'NONE', #11553, .T. ) ;
#18756=ADVANCED_FACE ( 'NONE', ( #7350 ), #21000, .T. ) ;
#18798=CIRCLE ( 'NONE', #21665, 2.076718556943725424 ) ;
#18808=CIRCLE ( 'NONE', #12001, 0.2500000000000002220 ) ;
#18845=VECTOR ( 'NONE', #9860, 1000.000000000000000 ) ;
#18868=EDGE_LOOP ( 'NONE', ( #14932, #19979, #906 ) ) ;
#18877=FACE_OUTER_BOUND ( 'NONE', #3908, .T. ) ;
#18897=ADVANCED_FACE ( 'NONE', ( #4317 ), #11129, .T. ) ;
#18898=CARTESIAN_POINT ( 'NONE',  ( -21.71259690522456154, 45.22582864897715638, 68.50000000000000000 ) ) ;
#18901=ORIENTED_EDGE ( 'NONE', *, *, #1574, .F. ) ;
#18927=CARTESIAN_POINT ( 'NONE',  ( -21.67365502786443088, 45.72430987248279166, 68.50000000000000000 ) ) ;
#18931=SPHERICAL_SURFACE ( 'NONE', #12788, 0.2500000000000000000 ) ;
#18945=( NAMED_UNIT ( * ) SI_UNIT ( $, .STERADIAN. ) SOLID_ANGLE_UNIT ( ) );
#19012=DIRECTION ( 'NONE',  ( -0.2309407893632113573, 0.9729678061520313781, 0.000000000000000000 ) ) ;
#19062=DIRECTION ( 'NONE',  ( 0.000000000000000000, 0.000000000000000000, 1.000000000000000000 ) ) ;
#19088=ADVANCED_FACE ( 'NONE', ( #6789 ), #17104, .T. ) ;
#19092=ADVANCED_FACE ( 'NONE', ( #15477 ), #1838, .F. ) ;
#19104=CARTESIAN_POINT ( 'NONE',  ( -32.23382792203229741, 83.71979900898287497, 13.75000000000000000 ) ) ;
#19105=DIRECTION ( 'NONE',  ( -0.000000000000000000, -0.000000000000000000, -1.000000000000000000 ) ) ;
#19151=CARTESIAN_POINT ( 'NONE',  ( -23.36078716634399655, 44.83461903493144973, 13.74999999999999822 ) ) ;
#19159=AXIS2_PLACEMENT_3D ( 'NONE', #2733, #6114, #4523 ) ;
#19188=TOROIDAL_SURFACE ( 'NONE', #11315, 2.767785046117003489, 0.2500000000000000000 ) ;
#19217=AXIS2_PLACEMENT_3D ( 'NONE', #11345, #16491, #14700 ) ;
#19242=ADVANCED_FACE ( 'NONE', ( #7322 ), #19188, .T. ) ;
#19257=ORIENTED_EDGE ( 'NONE', *, *, #15085, .F. ) ;
#19262=AXIS2_PLACEMENT_3D ( 'NONE', #13831, #19105, #8814 ) ;
#19287=EDGE_CURVE ( 'NONE', #2269, #20918, #5686, .T. ) ;
#19311=( GEOMETRIC_REPRESENTATION_CONTEXT ( 3 ) GLOBAL_UNCERTAINTY_ASSIGNED_CONTEXT ( ( #4620 ) ) GLOBAL_UNIT_ASSIGNED_CONTEXT ( ( #13765, #20625, #18945 ) ) REPRESENTATION_CONTEXT ( 'NONE', 'WORKASPACE' ) );
#19317=ORIENTED_EDGE ( 'NONE', *, *, #5973, .F. ) ;
#19363=CARTESIAN_POINT ( 'NONE',  ( -32.23382792203229741, 83.71979900898287497, 13.75000000000000000 ) ) ;
#19399=DIRECTION ( 'NONE',  ( 0.000000000000000000, -1.000000000000000000, 0.000000000000000000 ) ) ;
#19446=CYLINDRICAL_SURFACE ( 'NONE', #20721, 0.2499999999999985845 ) ;
#19483=CARTESIAN_POINT ( 'NONE',  ( -32.29156311937309454, 83.96304096052088539, 13.75000000000000000 ) ) ;
#19486=ORIENTED_EDGE ( 'NONE', *, *, #14541, .F. ) ;
#19498=CARTESIAN_POINT ( 'NONE',  ( -32.23382792203229741, 83.71979900898287497, 68.25000000000000000 ) ) ;
#19507=ORIENTED_EDGE ( 'NONE', *, *, #8347, .T. ) ;
#19517=TOROIDAL_SURFACE ( 'NONE', #2362, 2.076718556943726313, 0.2500000000000000000 ) ;
#19529=CARTESIAN_POINT ( 'NONE',  ( -31.26086011588027347, 83.95073979834609190, 13.75000000000000000 ) ) ;
#19540=ADVANCED_FACE ( 'NONE', ( #3612 ), #12528, .T. ) ;
#19541=AXIS2_PLACEMENT_3D ( 'NONE', #6600, #1770, #1309 ) ;
#19571=VECTOR ( 'NONE', #12499, 1000.000000000000114 ) ;
#19586=EDGE_CURVE ( 'NONE', #13584, #14169, #5960, .T. ) ;
#19604=LINE ( 'NONE', #4384, #20615 ) ;
#19612=EDGE_LOOP ( 'NONE', ( #14569, #17111, #6799, #4700 ) ) ;
#19614=ADVANCED_FACE ( 'NONE', ( #21512 ), #19517, .T. ) ;
#19619=SURFACE_STYLE_USAGE ( .BOTH. , #5981 ) ;
#19655=DIRECTION ( 'NONE',  ( -0.000000000000000000, -0.000000000000000000, 1.000000000000000000 ) ) ;
#19658=AXIS2_PLACEMENT_3D ( 'NONE', #2518, #8120, #938 ) ;
#19667=PLANE ( 'NONE',  #10620 ) ;
#19673=DIRECTION ( 'NONE',  ( -0.000000000000000000, -0.000000000000000000, -1.000000000000000000 ) ) ;
#19681=CARTESIAN_POINT ( 'NONE',  ( -23.13310673709249343, 45.37789868843801599, 13.50000000000000000 ) ) ;
#19685=CARTESIAN_POINT ( 'NONE',  ( -24.94594744299175915, 42.46645089659918426, 68.50000000000000000 ) ) ;
#19686=DIRECTION ( 'NONE',  ( 0.2309407893632116904, -0.9729678061520312671, 0.000000000000000000 ) ) ;
#19702=ORIENTED_EDGE ( 'NONE', *, *, #1733, .F. ) ;
#19725=SURFACE_SIDE_STYLE ('',( #6540 ) ) ;
#19741=DIRECTION ( 'NONE',  ( -1.000000000000000000, 0.000000000000000000, 0.000000000000000000 ) ) ;
#19751=CARTESIAN_POINT ( 'NONE',  ( -32.48382792203229741, 83.71979900898287497, 68.50000000000000000 ) ) ;
#19803=CIRCLE ( 'NONE', #11924, 0.5000000000000004441 ) ;
#19837=EDGE_CURVE ( 'NONE', #18477, #5820, #18808, .T. ) ;
#19844=DIRECTION ( 'NONE',  ( -6.751320378806396803E-15, -1.602473635475851075E-15, 1.000000000000000000 ) ) ;
#19957=( LENGTH_UNIT ( ) NAMED_UNIT ( * ) SI_UNIT ( .MILLI., .METRE. ) );
#19979=ORIENTED_EDGE ( 'NONE', *, *, #1725, .T. ) ;
#19994=ORIENTED_EDGE ( 'NONE', *, *, #936, .T. ) ;
#19999=DIRECTION ( 'NONE',  ( -0.9729678061520320442, -0.2309407893632090536, 0.000000000000000000 ) ) ;
#20011=EDGE_CURVE ( 'NONE', #18383, #5113, #8114, .T. ) ;
#20036=ORIENTED_EDGE ( 'NONE', *, *, #12619, .T. ) ;
#20047=EDGE_CURVE ( 'NONE', #8820, #18590, #15593, .T. ) ;
#20079=DIRECTION ( 'NONE',  ( 1.000000000000000000, 0.000000000000000000, 6.938893903907222067E-15 ) ) ;
#20122=DIRECTION ( 'NONE',  ( -1.000000000000000000, 0.000000000000000000, 0.000000000000000000 ) ) ;
#20154=CARTESIAN_POINT ( 'NONE',  ( -32.23382792203229741, 83.71979900898287497, 68.50000000000000000 ) ) ;
#20167=EDGE_CURVE ( 'NONE', #18383, #7934, #1303, .T. ) ;
#20169=EDGE_CURVE ( 'NONE', #18477, #10960, #1934, .T. ) ;
#20183=EDGE_CURVE ( 'NONE', #6210, #2269, #3105, .T. ) ;
#20186=DIRECTION ( 'NONE',  ( 0.8556185176499238043, 0.5176069476490315902, 0.000000000000000000 ) ) ;
#20215=DIRECTION ( 'NONE',  ( -1.000000000000000000, 0.000000000000000000, 0.000000000000000000 ) ) ;
#20241=DIRECTION ( 'NONE',  ( 0.000000000000000000, 0.000000000000000000, 1.000000000000000000 ) ) ;
#20278=AXIS2_PLACEMENT_3D ( 'NONE', #10077, #12065, #11952 ) ;
#20288=ADVANCED_FACE ( 'NONE', ( #7437 ), #14018, .T. ) ;
#20301=EDGE_CURVE ( 'NONE', #18477, #8820, #3598, .T. ) ;
#20312=DIRECTION ( 'NONE',  ( -0.2309407893632116904, 0.9729678061520312671, 0.000000000000000000 ) ) ;
#20342=ORIENTED_EDGE ( 'NONE', *, *, #18443, .F. ) ;
#20378=DIRECTION ( 'NONE',  ( -0.9729678061520345977, -0.2309407893631976461, 0.000000000000000000 ) ) ;
#20392=PRODUCT ( 'Flap', 'Flap', '', ( #12407 ) ) ;
#20435=CARTESIAN_POINT ( 'NONE',  ( -21.92816239687475743, 42.46645089659918426, 68.25000000000000000 ) ) ;
#20456=MANIFOLD_SOLID_BREP ( 'Stock-MAS-696-1', #16326 ) ;
#20497=FACE_OUTER_BOUND ( 'NONE', #15095, .T. ) ;
#20498=CARTESIAN_POINT ( 'NONE',  ( -23.37634868863050031, 45.32016349109721176, 13.74999999999999822 ) ) ;
#20499=EDGE_LOOP ( 'NONE', ( #11994, #16952, #9866, #9476 ) ) ;
#20512=EDGE_CURVE ( 'NONE', #16312, #573, #12861, .T. ) ;
#20520=VERTEX_POINT ( 'NONE', #4841 ) ;
#20522=DIRECTION ( 'NONE',  ( 0.2309407893631744979, -0.9729678061520400378, 0.000000000000000000 ) ) ;
#20526=ORIENTED_EDGE ( 'NONE', *, *, #18443, .T. ) ;
#20532=EDGE_CURVE ( 'NONE', #18590, #5820, #2515, .T. ) ;
#20538=CYLINDRICAL_SURFACE ( 'NONE', #674, 3.017785046117004377 ) ;
#20552=ORIENTED_EDGE ( 'NONE', *, *, #4482, .F. ) ;
#20587=ORIENTED_EDGE ( 'NONE', *, *, #3066, .F. ) ;
#20615=VECTOR ( 'NONE', #16113, 1000.000000000000000 ) ;
#20623=CARTESIAN_POINT ( 'NONE',  ( -21.92816239687475743, 42.46645089659918426, 13.74999999999999822 ) ) ;
#20625=( NAMED_UNIT ( * ) PLANE_ANGLE_UNIT ( ) SI_UNIT ( $, .RADIAN. ) );
#20644=CIRCLE ( 'NONE', #6355, 0.2499999999999985012 ) ;
#20656=CIRCLE ( 'NONE', #5996, 0.2500000000000002220 ) ;
#20721=AXIS2_PLACEMENT_3D ( 'NONE', #7832, #859, #4120 ) ;
#20744=CARTESIAN_POINT ( 'NONE',  ( -21.92816239687475743, 42.46645089659918426, 68.25000000000000000 ) ) ;
#20746=ORIENTED_EDGE ( 'NONE', *, *, #5282, .F. ) ;
#20806=DIRECTION ( 'NONE',  ( -1.000000000000000000, 0.000000000000000000, 0.000000000000000000 ) ) ;
#20814=VECTOR ( 'NONE', #5721, 1000.000000000000000 ) ;
#20821=DIRECTION ( 'NONE',  ( 0.000000000000000000, 0.000000000000000000, 1.000000000000000000 ) ) ;
#20844=DIRECTION ( 'NONE',  ( 0.000000000000000000, 0.000000000000000000, 1.000000000000000000 ) ) ;
#20862=ORIENTED_EDGE ( 'NONE', *, *, #21397, .F. ) ;
#20875=VERTEX_POINT ( 'NONE', #9856 ) ;
#20909=ORIENTED_EDGE ( 'NONE', *, *, #10719, .T. ) ;
#20918=VERTEX_POINT ( 'NONE', #13647 ) ;
#20940=AXIS2_PLACEMENT_3D ( 'NONE', #11356, #1164, #8009 ) ;
#20963=AXIS2_PLACEMENT_3D ( 'NONE', #9457, #7800, #9908 ) ;
#20981=AXIS2_PLACEMENT_3D ( 'NONE', #8337, #16936, #13788 ) ;
#21000=CYLINDRICAL_SURFACE ( 'NONE', #8169, 0.2500000000000001665 ) ;
#21010=CIRCLE ( 'NONE', #19217, 0.2500000000000002220 ) ;
#21024=EDGE_CURVE ( 'NONE', #5793, #16645, #12529, .T. ) ;
#21048=CARTESIAN_POINT ( 'NONE',  ( -21.92816239687475743, 42.46645089659918426, 13.74999999999999822 ) ) ;
#21093=EDGE_CURVE ( 'NONE', #20918, #1592, #7195, .T. ) ;
#21101=ORIENTED_EDGE ( 'NONE', *, *, #7693, .T. ) ;
#21104=FACE_OUTER_BOUND ( 'NONE', #2091, .T. ) ;
#21125=CARTESIAN_POINT ( 'NONE',  ( -21.67365502786443088, 45.72430987248279166, 13.74999999999999822 ) ) ;
#21142=AXIS2_PLACEMENT_3D ( 'NONE', #13817, #18647, #1630 ) ;
#21174=DIRECTION ( 'NONE',  ( -0.000000000000000000, -0.000000000000000000, -1.000000000000000000 ) ) ;
#21182=DIRECTION ( 'NONE',  ( 0.000000000000000000, 0.000000000000000000, 1.000000000000000000 ) ) ;
#21189=DIRECTION ( 'NONE',  ( -0.2309407893632117181, 0.9729678061520313781, 0.000000000000000000 ) ) ;
#21192=EDGE_LOOP ( 'NONE', ( #4514, #11221, #8768, #20526 ) ) ;
#21210=DIRECTION ( 'NONE',  ( -0.000000000000000000, -0.000000000000000000, -1.000000000000000000 ) ) ;
#21231=DIRECTION ( 'NONE',  ( 1.000000000000000000, 0.000000000000000000, 0.000000000000000000 ) ) ;
#21290=VECTOR ( 'NONE', #21388, 999.9999999999998863 ) ;
#21296=EDGE_LOOP ( 'NONE', ( #14257, #18631, #3313, #16924 ) ) ;
#21306=FILL_AREA_STYLE ('',( #14682 ) ) ;
#21342=ORIENTED_EDGE ( 'NONE', *, *, #11467, .F. ) ;
#21344=AXIS2_PLACEMENT_3D ( 'NONE', #11134, #16395, #2744 ) ;
#21364=CIRCLE ( 'NONE', #17780, 0.2500000000000011657 ) ;
#21384=CIRCLE ( 'NONE', #6025, 0.2500000000000002220 ) ;
#21386=ORIENTED_EDGE ( 'NONE', *, *, #16988, .F. ) ;
#21388=DIRECTION ( 'NONE',  ( 0.2309407893632117181, -0.9729678061520313781, -0.000000000000000000 ) ) ;
#21397=EDGE_CURVE ( 'NONE', #2663, #5552, #11834, .T. ) ;
#21426=AXIS2_PLACEMENT_3D ( 'NONE', #14243, #11416, #21840 ) ;
#21501=ORIENTED_EDGE ( 'NONE', *, *, #14731, .T. ) ;
#21506=VERTEX_POINT ( 'NONE', #9792 ) ;
#21512=FACE_OUTER_BOUND ( 'NONE', #11694, .T. ) ;
#21517=AXIS2_PLACEMENT_3D ( 'NONE', #3974, #19399, #11001 ) ;
#21561=VECTOR ( 'NONE', #3616, 1000.000000000000000 ) ;
#21581=EDGE_CURVE ( 'NONE', #7934, #818, #15372, .T. ) ;
#21596=DIRECTION ( 'NONE',  ( -1.000000000000000000, 0.000000000000000000, 0.000000000000000000 ) ) ;
#21599=ORIENTED_EDGE ( 'NONE', *, *, #6560, .T. ) ;
#21600=CARTESIAN_POINT ( 'NONE',  ( -21.69312596654449621, 45.47506926072997402, 13.74999999999999822 ) ) ;
#21614=ORIENTED_EDGE ( 'NONE', *, *, #10331, .T. ) ;
#21665=AXIS2_PLACEMENT_3D ( 'NONE', #7771, #6101, #2610 ) ;
#21668=EDGE_LOOP ( 'NONE', ( #12615, #17009, #16203, #16512 ) ) ;
#21703=EDGE_CURVE ( 'NONE', #9296, #1345, #11182, .T. ) ;
#21773=CARTESIAN_POINT ( 'NONE',  ( -10.48680304830625154, -2.489116863435002713, 68.50000000000000000 ) ) ;
#21798=ORIENTED_EDGE ( 'NONE', *, *, #14641, .T. ) ;
#21807=EDGE_LOOP ( 'NONE', ( #2282, #10605, #314, #11613, #6967, #16581, #22142, #7955 ) ) ;
#21817=LINE ( 'NONE', #15180, #6352 ) ;
#21840=DIRECTION ( 'NONE',  ( -1.000000000000000000, 0.000000000000000000, 0.000000000000000000 ) ) ;
#21849=DIRECTION ( 'NONE',  ( -0.000000000000000000, 0.000000000000000000, 1.000000000000000000 ) ) ;
#21865=DIRECTION ( 'NONE',  ( 0.000000000000000000, -0.000000000000000000, -1.000000000000000000 ) ) ;
#21884=EDGE_CURVE ( 'NONE', #10960, #17196, #4157, .T. ) ;
#21897=ORIENTED_EDGE ( 'NONE', *, *, #6389, .T. ) ;
#21912=CIRCLE ( 'NONE', #9746, 0.2500000000000002220 ) ;
#21914=ORIENTED_EDGE ( 'NONE', *, *, #936, .F. ) ;
#21924=CARTESIAN_POINT ( 'NONE',  ( -32.23382792203229741, 83.71979900898287497, 68.50000000000000000 ) ) ;
#21942=DIRECTION ( 'NONE',  ( -0.2309407893632008379, 0.9729678061520339316, 3.204947270951672174E-15 ) ) ;
#21957=DIRECTION ( 'NONE',  ( -1.000000000000000000, 0.000000000000000000, 0.000000000000000000 ) ) ;
#21973=CARTESIAN_POINT ( 'NONE',  ( -23.36959064016851073, 45.26242829375641463, 68.50000000000000000 ) ) ;
#21992=DIRECTION ( 'NONE',  ( 1.000000000000000000, 0.000000000000000000, 0.000000000000000000 ) ) ;
#21999=ORIENTED_EDGE ( 'NONE', *, *, #20011, .T. ) ;
#22030=DIRECTION ( 'NONE',  ( -0.9729678061520319332, -0.2309407893632090258, 0.000000000000000000 ) ) ;
#22077=ADVANCED_FACE ( 'NONE', ( #2147 ), #8981, .T. ) ;
#22113=CARTESIAN_POINT ( 'NONE',  ( -21.92816239687475743, 42.46645089659918426, 68.25000000000000000 ) ) ;
#22116=AXIS2_PLACEMENT_3D ( 'NONE', #13181, #9617, #11502 ) ;
#22121=DIRECTION ( 'NONE',  ( -0.9729678061520314891, -0.2309407893632107189, 0.000000000000000000 ) ) ;
#22142=ORIENTED_EDGE ( 'NONE', *, *, #9154, .T. ) ;
#22151=DIRECTION ( 'NONE',  ( 0.000000000000000000, 1.000000000000000000, -0.000000000000000000 ) ) ;
#22161=VERTEX_POINT ( 'NONE', #14560 ) ;
ENDSEC;
END-ISO-10303-21;
